ISO-10303-21;
HEADER;
FILE_DESCRIPTION (('STEP AP214'),
    '1' );
FILE_NAME ('hex flange nut_din_Hexagon Flange Nut DIN 6923 - M8 - S.step',
    '2026-10-09T14:04:53',
    ( '' ),
    ( '' ),
    'SwSTEP 2.0',
    'SolidWorks 2021',
    '' );
FILE_SCHEMA (( 'AUTOMOTIVE_DESIGN' ));
ENDSEC;

DATA;
#46=CARTESIAN_POINT ( 'NONE',  ( -5.978033218201116661, -4.054134411712217556, -0.5602453477493335443 ) ) ;
#95=AXIS2_PLACEMENT_3D ( 'NONE', #87472, #13552, #46470 ) ;
#112=VERTEX_POINT ( 'NONE', #1772 ) ;
#195=ORIENTED_EDGE ( 'NONE', *, *, #39067, .F. ) ;
#196=DIRECTION ( 'NONE',  ( 0.000000000000000000, 0.000000000000000000, 1.000000000000000000 ) ) ;
#268=EDGE_LOOP ( 'NONE', ( #80563, #62495, #21493, #73817, #21490 ) ) ;
#273=CARTESIAN_POINT ( 'NONE',  ( 4.444974277457670375, -4.939246403834011367, -5.720331885005380812 ) ) ;
#371=CYLINDRICAL_SURFACE ( 'NONE', #34798, 3.400000000000000355 ) ;
#384=DIRECTION ( 'NONE',  ( -1.000000000000000000, 0.000000000000000000, 0.000000000000000000 ) ) ;
#487=DIRECTION ( 'NONE',  ( -0.8191520442889881348, 1.003171929053520186E-16, 0.5735764363510513775 ) ) ;
#519=COLOUR_RGB ( '', 0.72549020, 0.75294118, 0.79215686) ;
#561=ORIENTED_EDGE ( 'NONE', *, *, #23670, .T. ) ;
#661=EDGE_CURVE ( 'NONE', #96379, #38000, #97654, .T. ) ;
#717=VERTEX_POINT ( 'NONE', #24779 ) ;
#722=DIRECTION ( 'NONE',  ( 0.8191520442889881348, 0.000000000000000000, 0.5735764363510513775 ) ) ;
#830=CARTESIAN_POINT ( 'NONE',  ( 3.400000000000000355, 0.000000000000000000, -2.716724522925831220 ) ) ;
#911=DIRECTION ( 'NONE',  ( 0.000000000000000000, 0.000000000000000000, 1.000000000000000000 ) ) ;
#1030=CONICAL_SURFACE ( 'NONE', #92299, 6.500000000000000888, 0.8987552595851637793 ) ;
#1038=CARTESIAN_POINT ( 'NONE',  ( 0.000000000000000000, 0.000000000000000000, -25.03750572909317285 ) ) ;
#1090=AXIS2_PLACEMENT_3D ( 'NONE', #64514, #23542, #89844 ) ;
#1109=AXIS2_PLACEMENT_3D ( 'NONE', #32248, #98025, #22039 ) ;
#1117=CARTESIAN_POINT ( 'NONE',  ( -5.441945782601306014, -4.363644636964944645, -0.3576316571898500163 ) ) ;
#1200=B_SPLINE_CURVE_WITH_KNOTS ( 'NONE', 3,
 ( #21077, #70646, #103540, #87370, #46370, #79260 ),
 .UNSPECIFIED., .F., .F.,
 ( 4, 2, 4 ),
 ( 8.673617379884035472E-19, 0.0003352299596267557021, 0.0006704599192535105369 ),
 .UNSPECIFIED. ) ;
#1245=DIRECTION ( 'NONE',  ( -0.000000000000000000, -0.000000000000000000, 1.000000000000000000 ) ) ;
#1264=DIRECTION ( 'NONE',  ( 1.000000000000000000, 0.000000000000000000, 0.000000000000000000 ) ) ;
#1271=CARTESIAN_POINT ( 'NONE',  ( -6.499999999999999112, -3.752776749732587902, -8.000000000000000000 ) ) ;
#1295=ADVANCED_FACE ( 'NONE', ( #85541 ), #13506, .F. ) ;
#1296=CARTESIAN_POINT ( 'NONE',  ( 6.499999999999996447, 1.286902272306400308, -0.09436334093185852478 ) ) ;
#1358=CARTESIAN_POINT ( 'NONE',  ( 0.000000000000000000, 0.000000000000000000, -1.161000000000000032 ) ) ;
#1446=ORIENTED_EDGE ( 'NONE', *, *, #35977, .F. ) ;
#1458=CARTESIAN_POINT ( 'NONE',  ( 3.400000000000000355, 0.000000000000000000, -3.852324522925831385 ) ) ;
#1488=EDGE_CURVE ( 'NONE', #96068, #80953, #103829, .T. ) ;
#1500=ORIENTED_EDGE ( 'NONE', *, *, #15313, .F. ) ;
#1586=DIRECTION ( 'NONE',  ( 0.000000000000000000, 0.000000000000000000, 1.000000000000000000 ) ) ;
#1641=DIRECTION ( 'NONE',  ( -1.000000000000000000, 0.000000000000000000, 0.000000000000000000 ) ) ;
#1717=TOROIDAL_SURFACE ( 'NONE', #91292, 8.331345277524542681, 0.6186547224754556096 ) ;
#1733=UNCERTAINTY_MEASURE_WITH_UNIT (LENGTH_MEASURE( 1.000000000000000082E-05 ), #70336, 'distance_accuracy_value', 'NONE');
#1734=CARTESIAN_POINT ( 'NONE',  ( -6.500000000000000888, 0.000000000000000000, 1.734723475976807094E-15 ) ) ;
#1765=CIRCLE ( 'NONE', #84495, 4.000000000000001776 ) ;
#1772=CARTESIAN_POINT ( 'NONE',  ( -4.000000000000000000, 0.000000000000000000, -4.567799999999999194 ) ) ;
#1810=ORIENTED_EDGE ( 'NONE', *, *, #86807, .F. ) ;
#1830=VECTOR ( 'NONE', #98914, 1000.000000000000114 ) ;
#1834=DIRECTION ( 'NONE',  ( -0.000000000000000000, -0.000000000000000000, -1.000000000000000000 ) ) ;
#1940=VECTOR ( 'NONE', #12867, 1000.000000000000000 ) ;
#1959=ORIENTED_EDGE ( 'NONE', *, *, #31611, .T. ) ;
#1966=DIRECTION ( 'NONE',  ( 1.000000000000000000, 0.000000000000000000, 0.000000000000000000 ) ) ;
#2004=DIRECTION ( 'NONE',  ( -1.000000000000000000, 0.000000000000000000, 0.000000000000000000 ) ) ;
#2166=CARTESIAN_POINT ( 'NONE',  ( 0.000000000000000000, 0.000000000000000000, -7.974599999999995248 ) ) ;
#2177=DIRECTION ( 'NONE',  ( -0.000000000000000000, -0.000000000000000000, -1.000000000000000000 ) ) ;
#2186=ORIENTED_EDGE ( 'NONE', *, *, #49857, .T. ) ;
#2196=EDGE_CURVE ( 'NONE', #71103, #717, #66791, .T. ) ;
#2204=CARTESIAN_POINT ( 'NONE',  ( -6.499999999999999112, 3.752776749732556816, -6.064240316920397333 ) ) ;
#2296=CYLINDRICAL_SURFACE ( 'NONE', #71585, 3.400000000000000355 ) ;
#2366=CONICAL_SURFACE ( 'NONE', #93703, 3.400000000000000355, 0.9599310885968748153 ) ;
#2381=CARTESIAN_POINT ( 'NONE',  ( -6.500000000000000000, -4.014037567183547317, -6.470355840301009742 ) ) ;
#2382=EDGE_LOOP ( 'NONE', ( #85674, #102561, #70360 ) ) ;
#2418=EDGE_CURVE ( 'NONE', #37530, #17654, #17641, .T. ) ;
#2499=ORIENTED_EDGE ( 'NONE', *, *, #52701, .F. ) ;
#2533=DIRECTION ( 'NONE',  ( 0.8191520442889881348, 0.000000000000000000, 0.5735764363510513775 ) ) ;
#2542=CARTESIAN_POINT ( 'NONE',  ( -6.837824896291514243, 3.947820044545419016, -6.564402953523714501 ) ) ;
#2561=AXIS2_PLACEMENT_3D ( 'NONE', #34284, #18629, #100571 ) ;
#2619=EDGE_CURVE ( 'NONE', #37787, #26114, #15366, .T. ) ;
#2663=DIRECTION ( 'NONE',  ( -0.000000000000000000, -0.000000000000000000, -1.000000000000000000 ) ) ;
#2724=DIRECTION ( 'NONE',  ( 0.000000000000000000, 0.000000000000000000, 1.000000000000000000 ) ) ;
#2769=DIRECTION ( 'NONE',  ( 0.000000000000000000, 0.000000000000000000, 1.000000000000000000 ) ) ;
#2812=AXIS2_PLACEMENT_3D ( 'NONE', #43526, #85046, #52129 ) ;
#2876=EDGE_LOOP ( 'NONE', ( #92110, #45201, #50312, #39231 ) ) ;
#2892=DIRECTION ( 'NONE',  ( -1.000000000000000000, 0.000000000000000000, 0.000000000000000000 ) ) ;
#2947=FACE_OUTER_BOUND ( 'NONE', #77757, .T. ) ;
#3023=DIRECTION ( 'NONE',  ( -1.000000000000000000, 0.000000000000000000, 0.000000000000000000 ) ) ;
#3068=SURFACE_STYLE_USAGE ( .BOTH. , #76954 ) ;
#3076=CARTESIAN_POINT ( 'NONE',  ( 5.619193549420741007, 4.261310591078456333, -5.875704392893664085 ) ) ;
#3142=CIRCLE ( 'NONE', #22098, 6.500000000000000000 ) ;
#3230=CARTESIAN_POINT ( 'NONE',  ( 4.366061277241470862, -4.984806845751398541, -0.09463688534108255501 ) ) ;
#3240=CARTESIAN_POINT ( 'NONE',  ( 5.007715329123895321E-16, -7.505553499465175804, -6.064240316920414209 ) ) ;
#3337=CARTESIAN_POINT ( 'NONE',  ( 2.837346585668846011, -6.232092946297409952, -6.171287963165208446 ) ) ;
#3379=CARTESIAN_POINT ( 'NONE',  ( 5.441945782601297132, 4.363644636964920664, -0.3576316571898332519 ) ) ;
#3454=DIRECTION ( 'NONE',  ( 1.000000000000000000, 0.000000000000000000, 0.000000000000000000 ) ) ;
#3463=ADVANCED_FACE ( 'NONE', ( #73197 ), #11445, .F. ) ;
#3478=( NAMED_UNIT ( * ) SI_UNIT ( $, .STERADIAN. ) SOLID_ANGLE_UNIT ( ) );
#3541=EDGE_CURVE ( 'NONE', #14549, #76235, #44691, .T. ) ;
#3561=EDGE_LOOP ( 'NONE', ( #67221, #106661, #62567, #61835 ) ) ;
#3576=AXIS2_PLACEMENT_3D ( 'NONE', #35319, #1834, #26180 ) ;
#3619=CARTESIAN_POINT ( 'NONE',  ( 0.8808064505792866372, 6.997019658119234542, -5.875704392893885242 ) ) ;
#3656=VERTEX_POINT ( 'NONE', #69847 ) ;
#3768=ORIENTED_EDGE ( 'NONE', *, *, #2418, .T. ) ;
#3769=CARTESIAN_POINT ( 'NONE',  ( 6.500000000000007105, -3.752776749732581685, -0.7999999999999977129 ) ) ;
#3817=EDGE_LOOP ( 'NONE', ( #102248, #67837, #10668 ) ) ;
#3850=CARTESIAN_POINT ( 'NONE',  ( 0.000000000000000000, 0.000000000000000000, -6.123524522925831270 ) ) ;
#3973=EDGE_LOOP ( 'NONE', ( #75321, #23575, #17516, #4423 ) ) ;
#3983=( GEOMETRIC_REPRESENTATION_CONTEXT ( 3 ) GLOBAL_UNCERTAINTY_ASSIGNED_CONTEXT ( ( #1733 ) ) GLOBAL_UNIT_ASSIGNED_CONTEXT ( ( #70336, #36937, #3478 ) ) REPRESENTATION_CONTEXT ( 'NONE', 'WORKASPACE' ) );
#4109=CONICAL_SURFACE ( 'NONE', #62621, 4.000000000000002665, 0.9599310885968824758 ) ;
#4147=FACE_OUTER_BOUND ( 'NONE', #67341, .T. ) ;
#4160=CARTESIAN_POINT ( 'NONE',  ( -0.5204879950542349309, -7.205049615410642261, -0.5609245978742314342 ) ) ;
#4252=DIRECTION ( 'NONE',  ( 0.000000000000000000, 0.000000000000000000, 1.000000000000000000 ) ) ;
#4292=ORIENTED_EDGE ( 'NONE', *, *, #79181, .F. ) ;
#4412=DIRECTION ( 'NONE',  ( 1.000000000000000000, 0.000000000000000000, 0.000000000000000000 ) ) ;
#4423=ORIENTED_EDGE ( 'NONE', *, *, #5283, .F. ) ;
#4426=ORIENTED_EDGE ( 'NONE', *, *, #66495, .F. ) ;
#4447=CARTESIAN_POINT ( 'NONE',  ( -6.269955739554010421, -4.268932597852962196, -6.443844059477448205 ) ) ;
#4591=EDGE_CURVE ( 'NONE', #87758, #56514, #97969, .T. ) ;
#4647=EDGE_LOOP ( 'NONE', ( #46310, #82931, #51409, #18473 ) ) ;
#4676=ADVANCED_FACE ( 'NONE', ( #41324 ), #80365, .F. ) ;
#4855=ADVANCED_FACE ( 'NONE', ( #50465 ), #101097, .T. ) ;
#4975=DIRECTION ( 'NONE',  ( 1.000000000000000000, 0.000000000000000000, 0.000000000000000000 ) ) ;
#5073=CARTESIAN_POINT ( 'NONE',  ( -6.499999999999999112, 3.752776749732556816, -6.064240316920397333 ) ) ;
#5100=DIRECTION ( 'NONE',  ( 0.000000000000000000, 0.000000000000000000, 1.000000000000000000 ) ) ;
#5134=ORIENTED_EDGE ( 'NONE', *, *, #102202, .F. ) ;
#5194=CIRCLE ( 'NONE', #86196, 4.000000000000000000 ) ;
#5209=CARTESIAN_POINT ( 'NONE',  ( 2.241046694639053261, 6.576374040526321352, -6.171384342982665139 ) ) ;
#5232=DIRECTION ( 'NONE',  ( -1.000000000000000000, 0.000000000000000000, 0.000000000000000000 ) ) ;
#5265=EDGE_CURVE ( 'NONE', #39998, #88814, #74617, .T. ) ;
#5283=EDGE_CURVE ( 'NONE', #94655, #112, #102630, .T. ) ;
#5325=CARTESIAN_POINT ( 'NONE',  ( -3.340000000000000746, 4.090320309152161009E-16, -0.4621369752184079083 ) ) ;
#5343=PLANE ( 'NONE',  #31462 ) ;
#5447=FACE_OUTER_BOUND ( 'NONE', #4647, .T. ) ;
#5463=DIRECTION ( 'NONE',  ( -0.000000000000000000, -0.000000000000000000, -1.000000000000000000 ) ) ;
#5468=VERTEX_POINT ( 'NONE', #60021 ) ;
#5543=EDGE_CURVE ( 'NONE', #23499, #100791, #71258, .T. ) ;
#5581=CARTESIAN_POINT ( 'NONE',  ( -3.400000000000000355, 4.163799117101001052E-16, -0.4455245229258316120 ) ) ;
#5675=ORIENTED_EDGE ( 'NONE', *, *, #48128, .F. ) ;
#5733=VECTOR ( 'NONE', #106496, 1000.000000000000000 ) ;
#5748=FACE_OUTER_BOUND ( 'NONE', #53867, .T. ) ;
#5757=DIRECTION ( 'NONE',  ( -1.000000000000000000, 0.000000000000000000, 0.000000000000000000 ) ) ;
#5773=VERTEX_POINT ( 'NONE', #8642 ) ;
#5821=DIRECTION ( 'NONE',  ( -1.000000000000000000, 0.000000000000000000, 0.000000000000000000 ) ) ;
#5863=DIRECTION ( 'NONE',  ( -1.000000000000000000, 0.000000000000000000, 0.000000000000000000 ) ) ;
#5892=ORIENTED_EDGE ( 'NONE', *, *, #85049, .T. ) ;
#5908=CARTESIAN_POINT ( 'NONE',  ( 0.000000000000000000, 0.000000000000000000, -8.000000000000000000 ) ) ;
#5928=EDGE_CURVE ( 'NONE', #72570, #54633, #8385, .T. ) ;
#5932=FACE_OUTER_BOUND ( 'NONE', #31424, .T. ) ;
#5965=CYLINDRICAL_SURFACE ( 'NONE', #20893, 3.400000000000000355 ) ;
#5998=AXIS2_PLACEMENT_3D ( 'NONE', #26334, #58106, #75892 ) ;
#6022=PRODUCT_DEFINITION_FORMATION_WITH_SPECIFIED_SOURCE ( 'ANY', '', #94105, .NOT_KNOWN. ) ;
#6040=ORIENTED_EDGE ( 'NONE', *, *, #42643, .F. ) ;
#6069=CARTESIAN_POINT ( 'NONE',  ( 6.499999999999999112, -3.752776749732586126, -6.064240316920402663 ) ) ;
#6135=CONICAL_SURFACE ( 'NONE', #54386, 6.500000000000000888, 0.8987552595851637793 ) ;
#6166=DIRECTION ( 'NONE',  ( -1.000000000000000000, 0.000000000000000000, 0.000000000000000000 ) ) ;
#6204=CARTESIAN_POINT ( 'NONE',  ( 6.500000000000000000, -0.6456425506958757277, 3.147574431996980060E-15 ) ) ;
#6247=FACE_OUTER_BOUND ( 'NONE', #18731, .T. ) ;
#6258=CARTESIAN_POINT ( 'NONE',  ( 0.000000000000000000, 0.000000000000000000, -6.123524522925831270 ) ) ;
#6284=DIRECTION ( 'NONE',  ( -1.000000000000000000, 0.000000000000000000, 0.000000000000000000 ) ) ;
#6332=EDGE_CURVE ( 'NONE', #17481, #96379, #86698, .T. ) ;
#6377=AXIS2_PLACEMENT_3D ( 'NONE', #73390, #90129, #39992 ) ;
#6404=ORIENTED_EDGE ( 'NONE', *, *, #6595, .F. ) ;
#6425=LINE ( 'NONE', #22662, #57718 ) ;
#6428=CARTESIAN_POINT ( 'NONE',  ( 8.542937654374686218, 0.000000000000000000, -6.800000000000000711 ) ) ;
#6595=EDGE_CURVE ( 'NONE', #19817, #37427, #56730, .T. ) ;
#6675=DIRECTION ( 'NONE',  ( 1.000000000000000000, 0.000000000000000000, 0.000000000000000000 ) ) ;
#6679=CARTESIAN_POINT ( 'NONE',  ( -3.397250002282850685E-16, 7.693909156114118630, -6.460786012260019362 ) ) ;
#6709=CIRCLE ( 'NONE', #56661, 0.6186547224754559426 ) ;
#6767=CIRCLE ( 'NONE', #91168, 4.000000000000000000 ) ;
#6814=CARTESIAN_POINT ( 'NONE',  ( 0.9108756637621119312, -6.979659189788956830, -6.219623095962687920 ) ) ;
#6827=CARTESIAN_POINT ( 'NONE',  ( 0.000000000000000000, 0.000000000000000000, -4.567799999999999194 ) ) ;
#6835=CARTESIAN_POINT ( 'NONE',  ( -3.400000000000000355, 4.163799117101001052E-16, -2.716724522925831220 ) ) ;
#6874=ORIENTED_EDGE ( 'NONE', *, *, #85049, .F. ) ;
#6883=CARTESIAN_POINT ( 'NONE',  ( 6.499999999999999112, 3.752776749732559036, -8.000000000000000000 ) ) ;
#6988=DIRECTION ( 'NONE',  ( -0.000000000000000000, -0.000000000000000000, -1.000000000000000000 ) ) ;
#7047=CARTESIAN_POINT ( 'NONE',  ( 6.500000000000600409, 0.6542365398605715088, -6.055391205187021342 ) ) ;
#7056=CARTESIAN_POINT ( 'NONE',  ( -4.000000000000000000, 0.000000000000000000, -2.296599999999999753 ) ) ;
#7080=EDGE_LOOP ( 'NONE', ( #105309, #27562, #18052 ) ) ;
#7100=ORIENTED_EDGE ( 'NONE', *, *, #18382, .F. ) ;
#7259=CARTESIAN_POINT ( 'NONE',  ( 0.000000000000000000, 0.000000000000000000, 1.734723475976807094E-15 ) ) ;
#7293=CARTESIAN_POINT ( 'NONE',  ( 4.000000000000000000, 4.898587196589412829E-16, -0.02540000000000007530 ) ) ;
#7335=CARTESIAN_POINT ( 'NONE',  ( 6.725979247667766003, -3.622307570260328902, -6.470294263593361350 ) ) ;
#7351=DIRECTION ( 'NONE',  ( -0.000000000000000000, -0.000000000000000000, -1.000000000000000000 ) ) ;
#7502=CARTESIAN_POINT ( 'NONE',  ( 6.818272094961328023, 1.321852500971151922, -6.208027553811806598 ) ) ;
#7549=EDGE_CURVE ( 'NONE', #76235, #87758, #9278, .T. ) ;
#7566=CARTESIAN_POINT ( 'NONE',  ( 6.500000000000000000, -2.723981882618820904, -6.224051986859710617 ) ) ;
#7584=CARTESIAN_POINT ( 'NONE',  ( 4.000000000000000000, 4.898587196589412829E-16, -1.161000000000000032 ) ) ;
#7614=EDGE_CURVE ( 'NONE', #35363, #102690, #19167, .T. ) ;
#7711=DIRECTION ( 'NONE',  ( 0.000000000000000000, 0.000000000000000000, 1.000000000000000000 ) ) ;
#7808=ORIENTED_EDGE ( 'NONE', *, *, #38803, .T. ) ;
#7964=DIRECTION ( 'NONE',  ( -0.5000000000000019984, -0.8660254037844374864, 0.000000000000000000 ) ) ;
#8049=CARTESIAN_POINT ( 'NONE',  ( -4.000000000000000000, 0.000000000000000000, -6.838999999999999524 ) ) ;
#8053=ORIENTED_EDGE ( 'NONE', *, *, #57855, .T. ) ;
#8140=PLANE ( 'NONE',  #15669 ) ;
#8141=FACE_OUTER_BOUND ( 'NONE', #14606, .T. ) ;
#8258=CIRCLE ( 'NONE', #87503, 4.000000000000000000 ) ;
#8281=DIRECTION ( 'NONE',  ( 0.8191520442889974607, 1.003171929053531649E-16, -0.5735764363510379438 ) ) ;
#8354=CARTESIAN_POINT ( 'NONE',  ( -6.746558653882563483, -3.895127454922790999, -6.526045885145577152 ) ) ;
#8385=CIRCLE ( 'NONE', #25689, 6.500000000000000000 ) ;
#8404=CARTESIAN_POINT ( 'NONE',  ( 0.8808064505786505904, -6.997019658119629781, -5.875704392893251082 ) ) ;
#8461=UNCERTAINTY_MEASURE_WITH_UNIT (LENGTH_MEASURE( 1.000000000000000082E-05 ), #21937, 'distance_accuracy_value', 'NONE');
#8549=EDGE_CURVE ( 'NONE', #112, #14702, #51183, .T. ) ;
#8642=CARTESIAN_POINT ( 'NONE',  ( -8.542937654374686218, 1.046208125374536008E-15, -6.800000000000000711 ) ) ;
#8662=EDGE_CURVE ( 'NONE', #17532, #67283, #85718, .T. ) ;
#8944=CIRCLE ( 'NONE', #84802, 4.000000000000000000 ) ;
#8953=EDGE_LOOP ( 'NONE', ( #29346, #56609, #36486, #53269 ) ) ;
#9032=CARTESIAN_POINT ( 'NONE',  ( 8.673617379884035472E-16, 7.505553499465148271, -0.7999999999999977129 ) ) ;
#9202=DIRECTION ( 'NONE',  ( -0.000000000000000000, -0.000000000000000000, -1.000000000000000000 ) ) ;
#9278=B_SPLINE_CURVE_WITH_KNOTS ( 'NONE', 3,
 ( #74182, #82280, #98460, #26228, #41295 ),
 .UNSPECIFIED., .F., .F.,
 ( 4, 1, 4 ),
 ( 0.000000000000000000, 0.003752776749732572668, 0.007505553499465145335 ),
 .UNSPECIFIED. ) ;
#9303=ORIENTED_EDGE ( 'NONE', *, *, #27591, .F. ) ;
#9352=DIRECTION ( 'NONE',  ( -0.000000000000000000, -0.000000000000000000, -1.000000000000000000 ) ) ;
#9394=DIRECTION ( 'NONE',  ( -0.000000000000000000, -0.000000000000000000, -1.000000000000000000 ) ) ;
#9488=VERTEX_POINT ( 'NONE', #50763 ) ;
#9541=CYLINDRICAL_SURFACE ( 'NONE', #35177, 3.400000000000000355 ) ;
#9613=CARTESIAN_POINT ( 'NONE',  ( 6.269955739554009533, 4.268932597852935551, -6.443844059477446429 ) ) ;
#9683=VECTOR ( 'NONE', #83251, 1000.000000000000000 ) ;
#9731=CARTESIAN_POINT ( 'NONE',  ( 0.000000000000000000, 0.000000000000000000, -0.7408754770741831086 ) ) ;
#9813=EDGE_LOOP ( 'NONE', ( #75618, #60759, #76375 ) ) ;
#9833=CARTESIAN_POINT ( 'NONE',  ( 3.250000000000015987, -5.629165124598843661, 1.734723475976807094E-15 ) ) ;
#9879=VERTEX_POINT ( 'NONE', #100140 ) ;
#10118=DIRECTION ( 'NONE',  ( -0.000000000000000000, -0.000000000000000000, 1.000000000000000000 ) ) ;
#10217=CIRCLE ( 'NONE', #68844, 3.400000000000000355 ) ;
#10271=DIRECTION ( 'NONE',  ( 0.000000000000000000, 0.000000000000000000, -1.000000000000000000 ) ) ;
#10280=CARTESIAN_POINT ( 'NONE',  ( 0.000000000000000000, 0.000000000000000000, -3.852324522925831385 ) ) ;
#10453=DIRECTION ( 'NONE',  ( -0.000000000000000000, -0.000000000000000000, -1.000000000000000000 ) ) ;
#10471=CARTESIAN_POINT ( 'NONE',  ( -6.499999999999998224, 2.723853875608233555, -6.224027332483752950 ) ) ;
#10494=EDGE_CURVE ( 'NONE', #76235, #29175, #94607, .T. ) ;
#10576=CARTESIAN_POINT ( 'NONE',  ( -6.499999999999999112, 3.752776749732556816, -6.064240316920397333 ) ) ;
#10581=ORIENTED_EDGE ( 'NONE', *, *, #99200, .T. ) ;
#10620=DIRECTION ( 'NONE',  ( 1.000000000000000000, 0.000000000000000000, 0.000000000000000000 ) ) ;
#10668=ORIENTED_EDGE ( 'NONE', *, *, #91480, .F. ) ;
#10687=ORIENTED_EDGE ( 'NONE', *, *, #68314, .T. ) ;
#10728=AXIS2_PLACEMENT_3D ( 'NONE', #14983, #57033, #47878 ) ;
#10764=CARTESIAN_POINT ( 'NONE',  ( 5.979512004945818582, -4.053280633787088583, -0.5609245978742307681 ) ) ;
#10770=VERTEX_POINT ( 'NONE', #58365 ) ;
#10880=COLOUR_RGB ( '', 0.72549020, 0.75294118, 0.79215686) ;
#10898=CARTESIAN_POINT ( 'NONE',  ( 0.000000000000000000, 0.000000000000000000, -3.432199999999999918 ) ) ;
#10969=LINE ( 'NONE', #86507, #45734 ) ;
#11095=DIRECTION ( 'NONE',  ( 0.000000000000000000, 0.000000000000000000, -1.000000000000000000 ) ) ;
#11145=DIRECTION ( 'NONE',  ( 1.000000000000000000, 0.000000000000000000, 0.000000000000000000 ) ) ;
#11189=DIRECTION ( 'NONE',  ( -0.000000000000000000, -0.000000000000000000, 1.000000000000000000 ) ) ;
#11223=EDGE_LOOP ( 'NONE', ( #46397, #60619, #63223, #45237 ) ) ;
#11319=ORIENTED_EDGE ( 'NONE', *, *, #44034, .T. ) ;
#11320=DIRECTION ( 'NONE',  ( 1.000000000000000000, 0.000000000000000000, 0.000000000000000000 ) ) ;
#11323=EDGE_LOOP ( 'NONE', ( #89265, #15557, #1959, #25535 ) ) ;
#11355=CARTESIAN_POINT ( 'NONE',  ( -6.746558653882650525, 3.895127454922563182, -6.526045885145563830 ) ) ;
#11356=EDGE_CURVE ( 'NONE', #102954, #104748, #55958, .T. ) ;
#11368=AXIS2_PLACEMENT_3D ( 'NONE', #46690, #74138, #90334 ) ;
#11396=ADVANCED_FACE ( 'NONE', ( #30146 ), #37236, .F. ) ;
#11425=VECTOR ( 'NONE', #40324, 1000.000000000000000 ) ;
#11437=VERTEX_POINT ( 'NONE', #27256 ) ;
#11445=CONICAL_SURFACE ( 'NONE', #1109, 4.000000000000000000, 0.9599310885968912466 ) ;
#11515=ORIENTED_EDGE ( 'NONE', *, *, #31994, .F. ) ;
#11527=CARTESIAN_POINT ( 'NONE',  ( -6.499999999999999112, -2.727365451014163167, -5.874157743772093987 ) ) ;
#11593=VERTEX_POINT ( 'NONE', #55912 ) ;
#11637=AXIS2_PLACEMENT_3D ( 'NONE', #29590, #61405, #62991 ) ;
#11694=CARTESIAN_POINT ( 'NONE',  ( -1.049032378834029666, -6.899894373156710614, -0.3607371497494648582 ) ) ;
#11717=VECTOR ( 'NONE', #50502, 1000.000000000000000 ) ;
#11780=CIRCLE ( 'NONE', #104804, 3.400000000000000355 ) ;
#11826=ADVANCED_FACE ( 'NONE', ( #92563 ), #6135, .T. ) ;
#11861=AXIS2_PLACEMENT_3D ( 'NONE', #18015, #101042, #43345 ) ;
#12033=ORIENTED_EDGE ( 'NONE', *, *, #4591, .T. ) ;
#12096=ORIENTED_EDGE ( 'NONE', *, *, #5928, .T. ) ;
#12136=EDGE_CURVE ( 'NONE', #37787, #102355, #39660, .T. ) ;
#12275=ORIENTED_EDGE ( 'NONE', *, *, #73735, .F. ) ;
#12419=LINE ( 'NONE', #103568, #103610 ) ;
#12495=VECTOR ( 'NONE', #13400, 1000.000000000000000 ) ;
#12538=EDGE_LOOP ( 'NONE', ( #103859, #88873, #29982, #47975 ) ) ;
#12571=DIRECTION ( 'NONE',  ( -0.000000000000000000, -0.000000000000000000, -1.000000000000000000 ) ) ;
#12594=ORIENTED_EDGE ( 'NONE', *, *, #79181, .T. ) ;
#12634=CARTESIAN_POINT ( 'NONE',  ( 0.2813450144774453654, -7.667988119308889239, -6.122077150241866939 ) ) ;
#12644=EDGE_LOOP ( 'NONE', ( #92912, #96560, #40310, #18296, #36493 ) ) ;
#12706=ADVANCED_FACE ( 'NONE', ( #38997 ), #51022, .F. ) ;
#12744=FILL_AREA_STYLE_COLOUR ( '', #519 ) ;
#12787=CARTESIAN_POINT ( 'NONE',  ( -12.99999999999996625, -1.778091562876227272E-14, 0.000000000000000000 ) ) ;
#12867=DIRECTION ( 'NONE',  ( -0.8191520442889881348, 1.003171929053520186E-16, 0.5735764363510513775 ) ) ;
#12905=CARTESIAN_POINT ( 'NONE',  ( -4.000000000000000000, 0.000000000000000000, -1.161000000000000032 ) ) ;
#12912=CIRCLE ( 'NONE', #73200, 3.400000000000000355 ) ;
#12956=DIRECTION ( 'NONE',  ( 1.000000000000000000, 0.000000000000000000, 0.000000000000000000 ) ) ;
#12963=FACE_OUTER_BOUND ( 'NONE', #55033, .T. ) ;
#12997=VECTOR ( 'NONE', #49466, 1000.000000000000000 ) ;
#12998=CARTESIAN_POINT ( 'NONE',  ( 6.826425371444816648, -2.641426549045784444, -6.344843397090118131 ) ) ;
#13092=CARTESIAN_POINT ( 'NONE',  ( 3.400000000000000355, 0.000000000000000000, -7.259124522925831435 ) ) ;
#13124=ORIENTED_EDGE ( 'NONE', *, *, #86157, .F. ) ;
#13134=FILL_AREA_STYLE_COLOUR ( '', #10880 ) ;
#13142=AXIS2_PLACEMENT_3D ( 'NONE', #46862, #79757, #5863 ) ;
#13153=DIRECTION ( 'NONE',  ( 1.000000000000000000, 0.000000000000000000, 0.000000000000000000 ) ) ;
#13201=AXIS2_PLACEMENT_3D ( 'NONE', #75749, #92458, #100552 ) ;
#13262=DIRECTION ( 'NONE',  ( -0.000000000000000000, -0.000000000000000000, 1.000000000000000000 ) ) ;
#13288=EDGE_CURVE ( 'NONE', #30156, #88814, #95559, .T. ) ;
#13316=FACE_OUTER_BOUND ( 'NONE', #7080, .T. ) ;
#13321=VERTEX_POINT ( 'NONE', #91038 ) ;
#13400=DIRECTION ( 'NONE',  ( -0.9396926207859142011, 0.000000000000000000, -0.3420201433256527812 ) ) ;
#13475=CARTESIAN_POINT ( 'NONE',  ( 4.000000000000000000, 4.898587196589412829E-16, -5.703399999999999359 ) ) ;
#13486=CARTESIAN_POINT ( 'NONE',  ( 4.000000000000000000, 4.898587196589412829E-16, -0.02540000000000007530 ) ) ;
#13506=CONICAL_SURFACE ( 'NONE', #32481, 4.000000000000000000, 0.9599310885968912466 ) ;
#13552=DIRECTION ( 'NONE',  ( 0.000000000000000000, 0.000000000000000000, -1.000000000000000000 ) ) ;
#13585=CARTESIAN_POINT ( 'NONE',  ( -3.978477517404915176, -5.573260695678979637, -6.171287963165205781 ) ) ;
#13672=( NAMED_UNIT ( * ) PLANE_ANGLE_UNIT ( ) SI_UNIT ( $, .RADIAN. ) );
#13740=CARTESIAN_POINT ( 'NONE',  ( -3.400000000000000355, 4.163799117101001052E-16, -6.418875477074183600 ) ) ;
#13789=ORIENTED_EDGE ( 'NONE', *, *, #46985, .T. ) ;
#13808=VECTOR ( 'NONE', #8281, 1000.000000000000114 ) ;
#13818=DIRECTION ( 'NONE',  ( -1.000000000000000000, 0.000000000000000000, 0.000000000000000000 ) ) ;
#13848=FACE_OUTER_BOUND ( 'NONE', #24543, .T. ) ;
#13854=ORIENTED_EDGE ( 'NONE', *, *, #70678, .T. ) ;
#13902=FACE_OUTER_BOUND ( 'NONE', #76896, .T. ) ;
#13953=FACE_OUTER_BOUND ( 'NONE', #53011, .T. ) ;
#13997=DIRECTION ( 'NONE',  ( 1.000000000000000000, 0.000000000000000000, 0.000000000000000000 ) ) ;
#14164=AXIS2_PLACEMENT_3D ( 'NONE', #26075, #50808, #32551 ) ;
#14231=DIRECTION ( 'NONE',  ( -1.000000000000000000, 0.000000000000000000, 0.000000000000000000 ) ) ;
#14296=EDGE_CURVE ( 'NONE', #76811, #54633, #50082, .T. ) ;
#14310=VERTEX_POINT ( 'NONE', #51882 ) ;
#14489=DIRECTION ( 'NONE',  ( -0.8191520442889974607, 0.000000000000000000, -0.5735764363510379438 ) ) ;
#14549=VERTEX_POINT ( 'NONE', #76572 ) ;
#14562=CONICAL_SURFACE ( 'NONE', #73077, 4.000000000000000000, 0.9599310885968912466 ) ;
#14569=STYLED_ITEM ( 'NONE', ( #53223 ), #17340 ) ;
#14594=CARTESIAN_POINT ( 'NONE',  ( 6.826575449902166248, 2.663085462279167093, -6.347418139105194257 ) ) ;
#14606=EDGE_LOOP ( 'NONE', ( #18212, #66803, #10687, #87043 ) ) ;
#14612=CARTESIAN_POINT ( 'NONE',  ( 1.083333333333333259, 6.880090707843052655, -5.848636054922040195 ) ) ;
#14687=CARTESIAN_POINT ( 'NONE',  ( 0.000000000000000000, 0.000000000000000000, -1.161000000000000032 ) ) ;
#14689=CIRCLE ( 'NONE', #74967, 3.400000000000000355 ) ;
#14702=VERTEX_POINT ( 'NONE', #58824 ) ;
#14751=EDGE_LOOP ( 'NONE', ( #94010, #37126, #54611, #59031 ) ) ;
#14755=CARTESIAN_POINT ( 'NONE',  ( -5.619193549420737455, -4.261310591078485643, -5.875704392893697836 ) ) ;
#14822=ORIENTED_EDGE ( 'NONE', *, *, #73922, .F. ) ;
#14883=DIRECTION ( 'NONE',  ( 0.000000000000000000, 0.000000000000000000, 1.000000000000000000 ) ) ;
#14916=ORIENTED_EDGE ( 'NONE', *, *, #26052, .F. ) ;
#14944=CONICAL_SURFACE ( 'NONE', #32223, 3.400000000000000355, 0.9599310885968748153 ) ;
#14956=ORIENTED_EDGE ( 'NONE', *, *, #80253, .F. ) ;
#14983=CARTESIAN_POINT ( 'NONE',  ( 0.000000000000000000, 0.000000000000000000, 0.000000000000000000 ) ) ;
#15002=EDGE_CURVE ( 'NONE', #717, #71103, #16629, .T. ) ;
#15046=ORIENTED_EDGE ( 'NONE', *, *, #45609, .F. ) ;
#15054=CARTESIAN_POINT ( 'NONE',  ( 6.500000000000000000, -2.501851166488394451, -5.848636054922037530 ) ) ;
#15058=CARTESIAN_POINT ( 'NONE',  ( 4.555094537983155334, 5.243183837310242623, -6.208110906918259175 ) ) ;
#15079=CARTESIAN_POINT ( 'NONE',  ( 6.815830331203685866, 0.6619522098568458857, -6.171384342982615401 ) ) ;
#15086=CARTESIAN_POINT ( 'NONE',  ( 0.000000000000000000, 0.000000000000000000, -0.4621369752184079083 ) ) ;
#15109=ORIENTED_EDGE ( 'NONE', *, *, #11356, .T. ) ;
#15131=CIRCLE ( 'NONE', #68505, 4.000000000000001776 ) ;
#15145=CARTESIAN_POINT ( 'NONE',  ( 6.818262094731102785, 1.323628772216710603, -6.207787212118526909 ) ) ;
#15313=EDGE_CURVE ( 'NONE', #96379, #70568, #95003, .T. ) ;
#15345=CARTESIAN_POINT ( 'NONE',  ( 0.000000000000000000, 0.000000000000000000, -7.554475477074167777 ) ) ;
#15366=LINE ( 'NONE', #23493, #70340 ) ;
#15453=ORIENTED_EDGE ( 'NONE', *, *, #15941, .F. ) ;
#15459=FACE_OUTER_BOUND ( 'NONE', #23982, .T. ) ;
#15539=ADVANCED_FACE ( 'NONE', ( #29288 ), #70765, .F. ) ;
#15557=ORIENTED_EDGE ( 'NONE', *, *, #88011, .T. ) ;
#15565=ORIENTED_EDGE ( 'NONE', *, *, #57855, .F. ) ;
#15570=CIRCLE ( 'NONE', #84511, 4.000000000000000000 ) ;
#15611=CYLINDRICAL_SURFACE ( 'NONE', #29312, 3.400000000000000355 ) ;
#15615=CARTESIAN_POINT ( 'NONE',  ( -6.818286579240214529, 1.325012739682868590, -6.208253321455268647 ) ) ;
#15669=AXIS2_PLACEMENT_3D ( 'NONE', #98729, #24885, #72864 ) ;
#15742=ADVANCED_FACE ( 'NONE', ( #8141 ), #23667, .F. ) ;
#15813=DIRECTION ( 'NONE',  ( 0.8191520442889974607, 1.003171929053531649E-16, -0.5735764363510379438 ) ) ;
#15859=VERTEX_POINT ( 'NONE', #78195 ) ;
#15931=CARTESIAN_POINT ( 'NONE',  ( 3.400000000000000355, 0.000000000000000000, -8.000000000000000000 ) ) ;
#15933=CARTESIAN_POINT ( 'NONE',  ( -6.837824896291514243, 3.947820044545419016, -6.564402953523714501 ) ) ;
#15941=EDGE_CURVE ( 'NONE', #54633, #64557, #44751, .T. ) ;
#15972=CARTESIAN_POINT ( 'NONE',  ( 5.589124336234602808, -4.278671059403162502, -6.219623095962701242 ) ) ;
#15997=ORIENTED_EDGE ( 'NONE', *, *, #101587, .T. ) ;
#16101=LINE ( 'NONE', #75071, #96510 ) ;
#16215=CARTESIAN_POINT ( 'NONE',  ( -3.400000000000000355, 4.163799117101001052E-16, -1.581124522925831499 ) ) ;
#16218=EDGE_LOOP ( 'NONE', ( #15997, #23239, #39573, #87353 ) ) ;
#16230=APPLICATION_CONTEXT ( 'automotive_design' ) ;
#16344=SHAPE_DEFINITION_REPRESENTATION ( #52755, #25516 ) ;
#16385=CIRCLE ( 'NONE', #64661, 3.400000000000000355 ) ;
#16432=ORIENTED_EDGE ( 'NONE', *, *, #93021, .T. ) ;
#16455=DIRECTION ( 'NONE',  ( 0.000000000000000000, 0.000000000000000000, 1.000000000000000000 ) ) ;
#16456=EDGE_CURVE ( 'NONE', #57008, #9879, #47482, .T. ) ;
#16617=CARTESIAN_POINT ( 'NONE',  ( 0.000000000000000000, 0.000000000000000000, -7.381345277524544279 ) ) ;
#16629=CIRCLE ( 'NONE', #95866, 3.400000000000000355 ) ;
#16709=AXIS2_PLACEMENT_3D ( 'NONE', #6827, #56427, #65071 ) ;
#16726=ORIENTED_EDGE ( 'NONE', *, *, #39067, .T. ) ;
#16797=AXIS2_PLACEMENT_3D ( 'NONE', #91916, #83290, #2892 ) ;
#16843=CARTESIAN_POINT ( 'NONE',  ( 0.000000000000000000, 0.000000000000000000, -7.974599999999995248 ) ) ;
#17052=VECTOR ( 'NONE', #64237, 1000.000000000000000 ) ;
#17062=CARTESIAN_POINT ( 'NONE',  ( 0.000000000000000000, 0.000000000000000000, 3.469446951953614189E-15 ) ) ;
#17066=CARTESIAN_POINT ( 'NONE',  ( 6.499999999999999112, -3.752776749732586126, -8.000000000000000000 ) ) ;
#17177=DIRECTION ( 'NONE',  ( 1.000000000000000000, 0.000000000000000000, 0.000000000000000000 ) ) ;
#17283=FACE_OUTER_BOUND ( 'NONE', #16218, .T. ) ;
#17299=CARTESIAN_POINT ( 'NONE',  ( 0.000000000000000000, 0.000000000000000000, -0.02540000000000007530 ) ) ;
#17340=MANIFOLD_SOLID_BREP ( 'ThdSchPat', #32555 ) ;
#17356=CARTESIAN_POINT ( 'NONE',  ( -4.358513833876425991, -4.989164364209899283, -0.07763482564822386800 ) ) ;
#17411=FACE_OUTER_BOUND ( 'NONE', #98495, .T. ) ;
#17417=ORIENTED_EDGE ( 'NONE', *, *, #27591, .T. ) ;
#17433=( BOUNDED_SURFACE ( )  B_SPLINE_SURFACE ( 3, 2, ( 
 ( #76959, #103884, #19321 ),
 ( #3076, #37076, #54254 ),
 ( #61872, #68896, #29520 ),
 ( #79086, #101769, #5209 ),
 ( #3619, #30031, #62920 ),
 ( #52148, #94220, #60799 ) ),
 .UNSPECIFIED., .F., .F., .F. ) 
 B_SPLINE_SURFACE_WITH_KNOTS ( ( 4, 2, 4 ),
 ( 3, 3 ),
 ( 0.003190620565844217750, 0.007281897438794487573, 0.01137317431174475826 ),
 ( 0.000000000000000000, 1.000000000000000000 ),
 .UNSPECIFIED. ) 
 GEOMETRIC_REPRESENTATION_ITEM ( )  RATIONAL_B_SPLINE_SURFACE ( (
 ( 1.000000000000000000, 0.8047731410850402778, 1.000000000000000000),
 ( 1.000000000000000000, 0.8125552299160839764, 1.000000000000000000),
 ( 1.000000000000000000, 0.8191520442883742925, 1.000000000000000000),
 ( 1.000000000000000000, 0.8191520442895997567, 1.000000000000000000),
 ( 1.000000000000000000, 0.8125552299151627134, 1.000000000000000000),
 ( 1.000000000000000000, 0.8047731410850398337, 1.000000000000000000) ) ) 
 REPRESENTATION_ITEM ( '' )  SURFACE ( )  );
#17481=VERTEX_POINT ( 'NONE', #15933 ) ;
#17516=ORIENTED_EDGE ( 'NONE', *, *, #31994, .T. ) ;
#17532=VERTEX_POINT ( 'NONE', #22475 ) ;
#17641=LINE ( 'NONE', #99591, #11717 ) ;
#17654=VERTEX_POINT ( 'NONE', #67682 ) ;
#17810=DIRECTION ( 'NONE',  ( 1.000000000000000000, 0.000000000000000000, 0.000000000000000000 ) ) ;
#17907=EDGE_CURVE ( 'NONE', #23499, #50026, #88510, .T. ) ;
#18002=ORIENTED_EDGE ( 'NONE', *, *, #15002, .F. ) ;
#18015=CARTESIAN_POINT ( 'NONE',  ( 0.000000000000000000, 0.000000000000000000, -4.567799999999999194 ) ) ;
#18052=ORIENTED_EDGE ( 'NONE', *, *, #104075, .F. ) ;
#18069=ORIENTED_EDGE ( 'NONE', *, *, #8662, .F. ) ;
#18142=ORIENTED_EDGE ( 'NONE', *, *, #68314, .F. ) ;
#18212=ORIENTED_EDGE ( 'NONE', *, *, #17907, .F. ) ;
#18223=ORIENTED_EDGE ( 'NONE', *, *, #93021, .F. ) ;
#18245=VERTEX_POINT ( 'NONE', #48431 ) ;
#18296=ORIENTED_EDGE ( 'NONE', *, *, #74743, .T. ) ;
#18368=DIRECTION ( 'NONE',  ( -1.000000000000000000, 0.000000000000000000, 0.000000000000000000 ) ) ;
#18370=CARTESIAN_POINT ( 'NONE',  ( 3.250000000000015987, -5.629165124598843661, 1.734723475976807094E-15 ) ) ;
#18382=EDGE_CURVE ( 'NONE', #72570, #25185, #68802, .T. ) ;
#18420=DIRECTION ( 'NONE',  ( 0.000000000000000000, 0.000000000000000000, 1.000000000000000000 ) ) ;
#18473=ORIENTED_EDGE ( 'NONE', *, *, #51879, .T. ) ;
#18551=DIRECTION ( 'NONE',  ( 0.5000000000000024425, -0.8660254037844372643, 0.000000000000000000 ) ) ;
#18558=CARTESIAN_POINT ( 'NONE',  ( 0.000000000000000000, 0.000000000000000000, -3.012075477074183105 ) ) ;
#18623=AXIS2_PLACEMENT_3D ( 'NONE', #54332, #69496, #103446 ) ;
#18629=DIRECTION ( 'NONE',  ( -0.000000000000000000, -0.000000000000000000, -1.000000000000000000 ) ) ;
#18636=ORIENTED_EDGE ( 'NONE', *, *, #104075, .T. ) ;
#18642=ORIENTED_EDGE ( 'NONE', *, *, #96032, .F. ) ;
#18656=AXIS2_PLACEMENT_3D ( 'NONE', #25633, #101068, #60114 ) ;
#18669=ORIENTED_EDGE ( 'NONE', *, *, #661, .T. ) ;
#18681=ORIENTED_EDGE ( 'NONE', *, *, #95545, .T. ) ;
#18712=CARTESIAN_POINT ( 'NONE',  ( -3.400000000000000355, 4.163799117101001052E-16, -8.000000000000000000 ) ) ;
#18731=EDGE_LOOP ( 'NONE', ( #12275, #5892, #16432, #71187 ) ) ;
#18766=CARTESIAN_POINT ( 'NONE',  ( 3.400000000000000355, 0.000000000000000000, -1.876475477074182940 ) ) ;
#18854=CARTESIAN_POINT ( 'NONE',  ( 0.000000000000000000, 0.000000000000000000, -8.000000000000000000 ) ) ;
#18921=VERTEX_POINT ( 'NONE', #105883 ) ;
#18947=EDGE_LOOP ( 'NONE', ( #18972, #96319, #12033, #18636, #51189 ) ) ;
#18950=ORIENTED_EDGE ( 'NONE', *, *, #88246, .F. ) ;
#18962=FACE_OUTER_BOUND ( 'NONE', #24028, .T. ) ;
#18970=DIRECTION ( 'NONE',  ( 1.000000000000000000, 0.000000000000000000, 0.000000000000000000 ) ) ;
#18972=ORIENTED_EDGE ( 'NONE', *, *, #10494, .F. ) ;
#19122=CONICAL_SURFACE ( 'NONE', #95, 4.000000000000002665, 0.9599310885968824758 ) ;
#19167=CIRCLE ( 'NONE', #69095, 6.500000000000000000 ) ;
#19321=CARTESIAN_POINT ( 'NONE',  ( 6.878751942472531411, 3.924677726130916255, -6.573129608219089093 ) ) ;
#19464=AXIS2_PLACEMENT_3D ( 'NONE', #63611, #65178, #99120 ) ;
#19473=ORIENTED_EDGE ( 'NONE', *, *, #84004, .F. ) ;
#19678=ORIENTED_EDGE ( 'NONE', *, *, #25782, .T. ) ;
#19690=CARTESIAN_POINT ( 'NONE',  ( -6.499999999998818723, -2.692912473540151286, -6.218066308271905207 ) ) ;
#19817=VERTEX_POINT ( 'NONE', #103825 ) ;
#19878=ORIENTED_EDGE ( 'NONE', *, *, #96851, .F. ) ;
#19953=ORIENTED_EDGE ( 'NONE', *, *, #29868, .T. ) ;
#20005=CARTESIAN_POINT ( 'NONE',  ( 4.000000000000001776, 0.000000000000000000, -8.000000000000000000 ) ) ;
#20076=FACE_OUTER_BOUND ( 'NONE', #95199, .T. ) ;
#20099=CARTESIAN_POINT ( 'NONE',  ( -6.499999999999999112, -3.752776749732595452, -0.7999999999999977129 ) ) ;
#20140=CARTESIAN_POINT ( 'NONE',  ( 4.358513833876418886, 4.989164364209876190, -0.07763482564820534115 ) ) ;
#20157=EDGE_CURVE ( 'NONE', #17481, #72013, #44134, .T. ) ;
#20274=CARTESIAN_POINT ( 'NONE',  ( -5.727634848077227225, 4.575561887448870380, -6.326622577870805841 ) ) ;
#20335=DIRECTION ( 'NONE',  ( 0.000000000000000000, 0.000000000000000000, 1.000000000000000000 ) ) ;
#20398=CARTESIAN_POINT ( 'NONE',  ( -2.133938722758583761, -6.273523403446334079, -0.09463688534108292971 ) ) ;
#20427=DIRECTION ( 'NONE',  ( 0.000000000000000000, 0.000000000000000000, 1.000000000000000000 ) ) ;
#20463=ORIENTED_EDGE ( 'NONE', *, *, #76970, .T. ) ;
#20478=ORIENTED_EDGE ( 'NONE', *, *, #49670, .F. ) ;
#20510=( BOUNDED_SURFACE ( )  B_SPLINE_SURFACE ( 3, 2, ( 
 ( #71410, #38034, #30459 ),
 ( #62814, #37508, #28343 ),
 ( #70896, #61769, #21315 ),
 ( #36970, #103785, #70371 ),
 ( #47136, #29928, #20274 ),
 ( #77929, #94665, #53125 ) ),
 .UNSPECIFIED., .F., .F., .F. ) 
 B_SPLINE_SURFACE_WITH_KNOTS ( ( 4, 2, 4 ),
 ( 3, 3 ),
 ( 0.003190620565844210377, 0.007281897438794483236, 0.01137317431174475653 ),
 ( 0.000000000000000000, 1.000000000000000000 ),
 .UNSPECIFIED. ) 
 GEOMETRIC_REPRESENTATION_ITEM ( )  RATIONAL_B_SPLINE_SURFACE ( (
 ( 1.000000000000000000, 0.8047731410850398337, 1.000000000000000000),
 ( 1.000000000000000000, 0.8125552299157385860, 1.000000000000000000),
 ( 1.000000000000000000, 0.8191520442888333697, 1.000000000000000000),
 ( 1.000000000000000000, 0.8191520442891397913, 1.000000000000000000),
 ( 1.000000000000000000, 0.8125552299155083258, 1.000000000000000000),
 ( 1.000000000000000000, 0.8047731410850402778, 1.000000000000000000) ) ) 
 REPRESENTATION_ITEM ( '' )  SURFACE ( )  );
#20556=ADVANCED_FACE ( 'NONE', ( #48247 ), #88266, .T. ) ;
#20560=ORIENTED_EDGE ( 'NONE', *, *, #98343, .T. ) ;
#20665=ORIENTED_EDGE ( 'NONE', *, *, #5265, .F. ) ;
#20709=CARTESIAN_POINT ( 'NONE',  ( -4.000000000000000000, 0.000000000000000000, -4.567799999999999194 ) ) ;
#20890=LINE ( 'NONE', #53724, #41434 ) ;
#20893=AXIS2_PLACEMENT_3D ( 'NONE', #102558, #61587, #94483 ) ;
#21064=ADVANCED_FACE ( 'NONE', ( #20076 ), #86674, .F. ) ;
#21077=CARTESIAN_POINT ( 'NONE',  ( 6.499999999999999112, 3.752776749732559036, -6.064240316920397333 ) ) ;
#21092=AXIS2_PLACEMENT_3D ( 'NONE', #7259, #40170, #71467 ) ;
#21137=ORIENTED_EDGE ( 'NONE', *, *, #90201, .F. ) ;
#21206=CARTESIAN_POINT ( 'NONE',  ( -6.837824896291513355, -3.947820044545450102, -6.564402953523720718 ) ) ;
#21268=CARTESIAN_POINT ( 'NONE',  ( -6.499999999999999112, 0.6470732608156783972, -0.01945970098672775497 ) ) ;
#21297=DIRECTION ( 'NONE',  ( -1.000000000000000000, 0.000000000000000000, 0.000000000000000000 ) ) ;
#21311=CARTESIAN_POINT ( 'NONE',  ( -5.727634848076409213, -4.575561887447700649, -6.326622577870337771 ) ) ;
#21315=CARTESIAN_POINT ( 'NONE',  ( -2.241046694639150960, 6.576374040526485665, -6.171384342982733529 ) ) ;
#21412=CARTESIAN_POINT ( 'NONE',  ( 0.000000000000000000, 0.000000000000000000, -8.000000000000000000 ) ) ;
#21414=CARTESIAN_POINT ( 'NONE',  ( 0.000000000000000000, 0.000000000000000000, -8.000000000000000000 ) ) ;
#21454=PLANE ( 'NONE',  #49803 ) ;
#21490=ORIENTED_EDGE ( 'NONE', *, *, #87375, .F. ) ;
#21493=ORIENTED_EDGE ( 'NONE', *, *, #20157, .F. ) ;
#21556=EDGE_CURVE ( 'NONE', #71103, #96068, #31725, .T. ) ;
#21597=DIRECTION ( 'NONE',  ( 0.8191520442889881348, 0.000000000000000000, 0.5735764363510513775 ) ) ;
#21739=ORIENTED_EDGE ( 'NONE', *, *, #75897, .F. ) ;
#21791=CARTESIAN_POINT ( 'NONE',  ( -6.499999999999999112, 3.752776749732556816, -0.7999999999999821698 ) ) ;
#21820=CIRCLE ( 'NONE', #32126, 3.981862520314373377 ) ;
#21840=CARTESIAN_POINT ( 'NONE',  ( -0.9108756637654614741, -6.979659189792516649, -6.219623095963290993 ) ) ;
#21909=CARTESIAN_POINT ( 'NONE',  ( 6.499999999999999112, -2.534234941938121821, -0.3584823952106133693 ) ) ;
#21922=EDGE_LOOP ( 'NONE', ( #79654, #28457, #53511, #71468 ) ) ;
#21937=( LENGTH_UNIT ( ) NAMED_UNIT ( * ) SI_UNIT ( .MILLI., .METRE. ) );
#22039=DIRECTION ( 'NONE',  ( -1.000000000000000000, 0.000000000000000000, 0.000000000000000000 ) ) ;
#22065=AXIS2_PLACEMENT_3D ( 'NONE', #100519, #196, #1264 ) ;
#22098=AXIS2_PLACEMENT_3D ( 'NONE', #79543, #71442, #30489 ) ;
#22240=CARTESIAN_POINT ( 'NONE',  ( 3.250000000000015099, 5.629165124598843661, 1.734723475976807094E-15 ) ) ;
#22272=B_SPLINE_CURVE_WITH_KNOTS ( 'NONE', 3,
 ( #65231, #98123, #41481, #91122, #74369, #72259 ),
 .UNSPECIFIED., .F., .F.,
 ( 4, 2, 4 ),
 ( 0.000000000000000000, 0.0003352299596267586295, 0.0006704599192535172589 ),
 .UNSPECIFIED. ) ;
#22299=CARTESIAN_POINT ( 'NONE',  ( 6.500000000000005329, -3.752776749732582573, -6.177805531629061875 ) ) ;
#22374=CARTESIAN_POINT ( 'NONE',  ( -6.878751942472529635, -3.924677726130946009, -6.573129608219094422 ) ) ;
#22475=CARTESIAN_POINT ( 'NONE',  ( -3.400000000000000355, 4.163799117101001052E-16, -1.876475477074182940 ) ) ;
#22531=ORIENTED_EDGE ( 'NONE', *, *, #69165, .T. ) ;
#22662=CARTESIAN_POINT ( 'NONE',  ( -3.400000000000000355, 4.163799117101001052E-16, -7.259124522925831435 ) ) ;
#22681=CARTESIAN_POINT ( 'NONE',  ( 6.837824896291514243, 3.947820044545422569, -6.564402953523715389 ) ) ;
#22779=EDGE_CURVE ( 'NONE', #17532, #3656, #10969, .T. ) ;
#22786=CARTESIAN_POINT ( 'NONE',  ( -2.832728918602883450, -6.234773369952756106, -6.171481112545262881 ) ) ;
#22818=ORIENTED_EDGE ( 'NONE', *, *, #95168, .F. ) ;
#22912=DIRECTION ( 'NONE',  ( -1.000000000000000000, 0.000000000000000000, 0.000000000000000000 ) ) ;
#22968=ORIENTED_EDGE ( 'NONE', *, *, #74725, .T. ) ;
#23005=CARTESIAN_POINT ( 'NONE',  ( -2.263183130831067924, 6.566419505188279437, -6.208110906918260952 ) ) ;
#23028=ORIENTED_EDGE ( 'NONE', *, *, #49698, .T. ) ;
#23076=EDGE_LOOP ( 'NONE', ( #27578, #27723, #22968, #87690 ) ) ;
#23180=CARTESIAN_POINT ( 'NONE',  ( 6.499999999999999112, -3.752776749732586126, -6.064240316920402663 ) ) ;
#23184=CARTESIAN_POINT ( 'NONE',  ( 3.978477517404916064, 5.573260695678952104, -6.171287963165197787 ) ) ;
#23239=ORIENTED_EDGE ( 'NONE', *, *, #16456, .T. ) ;
#23253=ORIENTED_EDGE ( 'NONE', *, *, #87585, .F. ) ;
#23493=CARTESIAN_POINT ( 'NONE',  ( 3.400000000000000355, 0.000000000000000000, -8.000000000000000000 ) ) ;
#23499=VERTEX_POINT ( 'NONE', #93660 ) ;
#23517=AXIS2_PLACEMENT_3D ( 'NONE', #29488, #38108, #87163 ) ;
#23542=DIRECTION ( 'NONE',  ( 0.000000000000000000, 0.000000000000000000, 1.000000000000000000 ) ) ;
#23575=ORIENTED_EDGE ( 'NONE', *, *, #72818, .T. ) ;
#23578=CARTESIAN_POINT ( 'NONE',  ( 0.000000000000000000, 0.000000000000000000, 1.734723475976807094E-15 ) ) ;
#23585=AXIS2_PLACEMENT_3D ( 'NONE', #26785, #67738, #101698 ) ;
#23613=ORIENTED_EDGE ( 'NONE', *, *, #5928, .F. ) ;
#23667=CONICAL_SURFACE ( 'NONE', #6377, 4.000000000000000000, 0.9599310885968912466 ) ;
#23670=EDGE_CURVE ( 'NONE', #5773, #37427, #44197, .T. ) ;
#23743=DIRECTION ( 'NONE',  ( 0.000000000000000000, 0.000000000000000000, 1.000000000000000000 ) ) ;
#23922=CONICAL_SURFACE ( 'NONE', #34305, 3.400000000000000355, 0.9599310885968748153 ) ;
#23942=( BOUNDED_SURFACE ( )  B_SPLINE_SURFACE ( 3, 2, ( 
 ( #84382, #93545, #35326 ),
 ( #43915, #10471, #34260 ),
 ( #26187, #76802, #60133 ),
 ( #75745, #67132, #42311 ),
 ( #11527, #19690, #92996 ),
 ( #69274, #2381, #84911 ) ),
 .UNSPECIFIED., .F., .F., .T. ) 
 B_SPLINE_SURFACE_WITH_KNOTS ( ( 4, 2, 4 ),
 ( 3, 3 ),
 ( 0.03172058138205609973, 0.03571597378202084894, 0.03971136618198560508 ),
 ( 0.000000000000000000, 1.000000000000000000 ),
 .UNSPECIFIED. ) 
 GEOMETRIC_REPRESENTATION_ITEM ( )  RATIONAL_B_SPLINE_SURFACE ( (
 ( 1.000000000000000000, 0.8047780791350978014, 1.000000000000000000),
 ( 1.000000000000000000, 0.8123796029720886658, 1.000000000000000000),
 ( 1.000000000000000000, 0.8190681660672747277, 1.000000000000000000),
 ( 1.000000000000000000, 0.8192342536573682388, 1.000000000000000000),
 ( 1.000000000000000000, 0.8126124427163601283, 1.000000000000000000),
 ( 1.000000000000000000, 0.8047712715942065831, 1.000000000000000000) ) ) 
 REPRESENTATION_ITEM ( '' )  SURFACE ( )  );
#23982=EDGE_LOOP ( 'NONE', ( #48901, #57571, #7100 ) ) ;
#24028=EDGE_LOOP ( 'NONE', ( #67486, #16726, #57219, #35315 ) ) ;
#24334=ADVANCED_FACE ( 'NONE', ( #5447 ), #104614, .F. ) ;
#24346=FACE_OUTER_BOUND ( 'NONE', #103085, .T. ) ;
#24424=ORIENTED_EDGE ( 'NONE', *, *, #93899, .T. ) ;
#24543=EDGE_LOOP ( 'NONE', ( #28497, #7808, #57613, #12096, #44653, #86501 ) ) ;
#24582=ORIENTED_EDGE ( 'NONE', *, *, #75897, .T. ) ;
#24583=DIRECTION ( 'NONE',  ( -0.000000000000000000, -0.000000000000000000, -1.000000000000000000 ) ) ;
#24626=CARTESIAN_POINT ( 'NONE',  ( 6.781345014477442312, -3.590342129888872691, -6.122077150241854504 ) ) ;
#24676=CONICAL_SURFACE ( 'NONE', #60847, 4.000000000000000000, 0.9599310885968912466 ) ;
#24724=DIRECTION ( 'NONE',  ( -0.000000000000000000, -0.000000000000000000, -1.000000000000000000 ) ) ;
#24779=CARTESIAN_POINT ( 'NONE',  ( 3.400000000000000355, 0.000000000000000000, -6.418875477074183600 ) ) ;
#24789=CARTESIAN_POINT ( 'NONE',  ( -3.250000000000013767, -5.629165124598844550, 1.734723475976807094E-15 ) ) ;
#24885=DIRECTION ( 'NONE',  ( 0.5000000000000022204, 0.8660254037844374864, -0.000000000000000000 ) ) ;
#24980=CARTESIAN_POINT ( 'NONE',  ( 0.000000000000000000, 0.000000000000000000, -8.000000000000000000 ) ) ;
#25158=CARTESIAN_POINT ( 'NONE',  ( -0.2259792476677738859, -7.636022678937434804, -6.470294263593375561 ) ) ;
#25185=VERTEX_POINT ( 'NONE', #106421 ) ;
#25260=CARTESIAN_POINT ( 'NONE',  ( 0.000000000000000000, 0.000000000000000000, -1.161000000000000032 ) ) ;
#25279=VECTOR ( 'NONE', #55622, 1000.000000000000000 ) ;
#25284=CARTESIAN_POINT ( 'NONE',  ( 0.000000000000000000, 0.000000000000000000, -8.000000000000000000 ) ) ;
#25296=CARTESIAN_POINT ( 'NONE',  ( -3.811597179862317830, 5.304926841629206358, -0.01956314070068032943 ) ) ;
#25389=VERTEX_POINT ( 'NONE', #104711 ) ;
#25448=ORIENTED_EDGE ( 'NONE', *, *, #47726, .F. ) ;
#25460=CIRCLE ( 'NONE', #16797, 3.400000000000000355 ) ;
#25516=SHAPE_REPRESENTATION ( 'hex flange nut_din_Hexagon Flange Nut DIN 6923 - M8 - S', ( #10728 ), #3983 ) ;
#25526=ORIENTED_EDGE ( 'NONE', *, *, #31589, .F. ) ;
#25535=ORIENTED_EDGE ( 'NONE', *, *, #74814, .F. ) ;
#25633=CARTESIAN_POINT ( 'NONE',  ( 0.000000000000000000, 0.000000000000000000, -6.838999999999999524 ) ) ;
#25649=CARTESIAN_POINT ( 'NONE',  ( 6.500000000000000000, 0.3213925021621148459, 3.091246741004567904E-15 ) ) ;
#25689=AXIS2_PLACEMENT_3D ( 'NONE', #47380, #40890, #106133 ) ;
#25711=CARTESIAN_POINT ( 'NONE',  ( -0.2813450144774510275, -7.667988119308891903, -6.122077150241868715 ) ) ;
#25727=DIRECTION ( 'NONE',  ( 1.000000000000000000, 0.000000000000000000, 0.000000000000000000 ) ) ;
#25782=EDGE_CURVE ( 'NONE', #13321, #86116, #104580, .T. ) ;
#25791=LINE ( 'NONE', #100153, #12997 ) ;
#25847=ORIENTED_EDGE ( 'NONE', *, *, #13288, .F. ) ;
#25851=CARTESIAN_POINT ( 'NONE',  ( -5.450967621166013188, 4.358435876040994472, -0.3607371497494452073 ) ) ;
#25921=EDGE_LOOP ( 'NONE', ( #51729, #22818, #3768, #98338 ) ) ;
#25939=DIRECTION ( 'NONE',  ( 1.000000000000000000, 0.000000000000000000, 0.000000000000000000 ) ) ;
#25995=CARTESIAN_POINT ( 'NONE',  ( -6.831979103402613163, -3.295157223185851691, -6.443785395948810724 ) ) ;
#26027=DIRECTION ( 'NONE',  ( 0.9396926207859142011, 1.150791560227857419E-16, -0.3420201433256527812 ) ) ;
#26052=EDGE_CURVE ( 'NONE', #64557, #72570, #82216, .T. ) ;
#26075=CARTESIAN_POINT ( 'NONE',  ( 0.000000000000000000, 0.000000000000000000, 1.734723475976807094E-15 ) ) ;
#26079=CARTESIAN_POINT ( 'NONE',  ( -6.500000000000000000, -3.155218591052693977, -0.5622968210053880256 ) ) ;
#26114=VERTEX_POINT ( 'NONE', #32318 ) ;
#26176=EDGE_LOOP ( 'NONE', ( #8053, #26807, #93005, #77891 ) ) ;
#26180=DIRECTION ( 'NONE',  ( -1.000000000000000000, 0.000000000000000000, 0.000000000000000000 ) ) ;
#26187=CARTESIAN_POINT ( 'NONE',  ( -6.499999999999999112, 1.416734669067071017, -5.722373386996367550 ) ) ;
#26228=CARTESIAN_POINT ( 'NONE',  ( 5.416666666666666963, -4.378239541354686182, -5.848636054922042860 ) ) ;
#26262=VERTEX_POINT ( 'NONE', #105000 ) ;
#26272=ORIENTED_EDGE ( 'NONE', *, *, #93262, .T. ) ;
#26334=CARTESIAN_POINT ( 'NONE',  ( 0.000000000000000000, 0.000000000000000000, -7.259124522925831435 ) ) ;
#26480=( GEOMETRIC_REPRESENTATION_CONTEXT ( 3 ) GLOBAL_UNCERTAINTY_ASSIGNED_CONTEXT ( ( #8461 ) ) GLOBAL_UNIT_ASSIGNED_CONTEXT ( ( #21937, #86146, #69937 ) ) REPRESENTATION_CONTEXT ( 'NONE', 'WORKASPACE' ) );
#26529=VERTEX_POINT ( 'NONE', #105402 ) ;
#26551=B_SPLINE_CURVE_WITH_KNOTS ( 'NONE', 3,
 ( #81399, #73308, #15615, #90041, #56599, #31827 ),
 .UNSPECIFIED., .F., .F.,
 ( 4, 2, 4 ),
 ( 0.003981881017442843659, 0.005970145066490154147, 0.007958409115537464634 ),
 .UNSPECIFIED. ) ;
#26765=CARTESIAN_POINT ( 'NONE',  ( -1.083333333333332593, -6.880090707843076636, -5.848636054922048189 ) ) ;
#26785=CARTESIAN_POINT ( 'NONE',  ( 0.000000000000000000, 0.000000000000000000, -6.800000000000000711 ) ) ;
#26807=ORIENTED_EDGE ( 'NONE', *, *, #90182, .T. ) ;
#26869=CARTESIAN_POINT ( 'NONE',  ( -6.270061300899935297, 4.268872906156492952, -6.443866470201758290 ) ) ;
#26875=CARTESIAN_POINT ( 'NONE',  ( 3.400000000000000355, 0.000000000000000000, -1.581124522925831499 ) ) ;
#26945=DIRECTION ( 'NONE',  ( 0.000000000000000000, 0.000000000000000000, 1.000000000000000000 ) ) ;
#26947=ORIENTED_EDGE ( 'NONE', *, *, #65905, .T. ) ;
#27119=CARTESIAN_POINT ( 'NONE',  ( 6.837824896291513355, -3.947820044545448326, -6.564402953523719830 ) ) ;
#27245=CARTESIAN_POINT ( 'NONE',  ( 6.500000000000000888, 0.000000000000000000, 1.734723475976807094E-15 ) ) ;
#27256=CARTESIAN_POINT ( 'NONE',  ( 6.837824896291513355, -3.947820044545448326, -6.564402953523719830 ) ) ;
#27328=AXIS2_PLACEMENT_3D ( 'NONE', #39396, #72274, #56057 ) ;
#27489=VERTEX_POINT ( 'NONE', #64960 ) ;
#27496=AXIS2_PLACEMENT_3D ( 'NONE', #56305, #9352, #31560 ) ;
#27530=DIRECTION ( 'NONE',  ( -0.8660254037844371533, -0.5000000000000025535, 0.000000000000000000 ) ) ;
#27562=ORIENTED_EDGE ( 'NONE', *, *, #7614, .F. ) ;
#27578=ORIENTED_EDGE ( 'NONE', *, *, #100772, .F. ) ;
#27591=EDGE_CURVE ( 'NONE', #39998, #5468, #37674, .T. ) ;
#27629=DIRECTION ( 'NONE',  ( -0.000000000000000000, -0.000000000000000000, -1.000000000000000000 ) ) ;
#27634=CIRCLE ( 'NONE', #93112, 3.400000000000000355 ) ;
#27662=CARTESIAN_POINT ( 'NONE',  ( 1.049032378833995693, 6.899894373156700844, -0.3607371497494533674 ) ) ;
#27723=ORIENTED_EDGE ( 'NONE', *, *, #66495, .T. ) ;
#27837=CARTESIAN_POINT ( 'NONE',  ( -3.249999999999999112, -5.629165124598882741, -5.592027715088716988 ) ) ;
#27875=AXIS2_PLACEMENT_3D ( 'NONE', #93661, #34388, #1966 ) ;
#27884=AXIS2_PLACEMENT_3D ( 'NONE', #99105, #911, #82939 ) ;
#27971=AXIS2_PLACEMENT_3D ( 'NONE', #38670, #86172, #5232 ) ;
#27979=ORIENTED_EDGE ( 'NONE', *, *, #35238, .T. ) ;
#28044=CARTESIAN_POINT ( 'NONE',  ( -4.000000000000000000, 0.000000000000000000, -6.838999999999999524 ) ) ;
#28086=VERTEX_POINT ( 'NONE', #74775 ) ;
#28135=CARTESIAN_POINT ( 'NONE',  ( -6.500000000000007105, 3.752776749732553707, -6.177802698399951886 ) ) ;
#28343=CARTESIAN_POINT ( 'NONE',  ( -1.098735407080559279, 7.248058225761153217, -6.326622577871103381 ) ) ;
#28351=DIRECTION ( 'NONE',  ( -1.000000000000000000, 0.000000000000000000, 0.000000000000000000 ) ) ;
#28416=ORIENTED_EDGE ( 'NONE', *, *, #20157, .T. ) ;
#28457=ORIENTED_EDGE ( 'NONE', *, *, #36837, .F. ) ;
#28497=ORIENTED_EDGE ( 'NONE', *, *, #7614, .T. ) ;
#28522=AXIS2_PLACEMENT_3D ( 'NONE', #9731, #9202, #1641 ) ;
#28570=CARTESIAN_POINT ( 'NONE',  ( -3.400000000000000355, 4.163799117101001052E-16, -4.987924522925830217 ) ) ;
#28615=DIRECTION ( 'NONE',  ( -1.000000000000000000, 0.000000000000000000, 0.000000000000000000 ) ) ;
#28656=LINE ( 'NONE', #35690, #57992 ) ;
#28711=CARTESIAN_POINT ( 'NONE',  ( 4.555432764205790797, -5.242992371775952343, -6.208169345099798342 ) ) ;
#28715=CARTESIAN_POINT ( 'NONE',  ( 0.5204879950541950739, 7.205049615410636044, -0.5609245978742248839 ) ) ;
#28716=DIRECTION ( 'NONE',  ( -1.000000000000000000, 0.000000000000000000, 0.000000000000000000 ) ) ;
#28741=ADVANCED_FACE ( 'NONE', ( #29959 ), #14944, .F. ) ;
#28761=CARTESIAN_POINT ( 'NONE',  ( 0.000000000000000000, 0.000000000000000000, -4.987924522925830217 ) ) ;
#28768=ORIENTED_EDGE ( 'NONE', *, *, #77774, .T. ) ;
#28776=CARTESIAN_POINT ( 'NONE',  ( -0.5619217318086657809, -7.564468822943342552, -6.443866470201776053 ) ) ;
#28838=DIRECTION ( 'NONE',  ( 0.000000000000000000, 0.000000000000000000, 1.000000000000000000 ) ) ;
#28910=ORIENTED_EDGE ( 'NONE', *, *, #38555, .T. ) ;
#28920=FACE_OUTER_BOUND ( 'NONE', #14751, .T. ) ;
#29092=EDGE_LOOP ( 'NONE', ( #25526, #71995, #99182, #74564 ) ) ;
#29175=VERTEX_POINT ( 'NONE', #43858 ) ;
#29207=DIRECTION ( 'NONE',  ( -0.000000000000000000, -0.000000000000000000, 1.000000000000000000 ) ) ;
#29254=CARTESIAN_POINT ( 'NONE',  ( 2.133938722758562001, 6.273523403446319868, -0.09463688534106554084 ) ) ;
#29288=FACE_OUTER_BOUND ( 'NONE', #43104, .T. ) ;
#29312=AXIS2_PLACEMENT_3D ( 'NONE', #97577, #23743, #81928 ) ;
#29339=CARTESIAN_POINT ( 'NONE',  ( 6.837824896291513355, -3.947820044545448326, -6.564402953523719830 ) ) ;
#29346=ORIENTED_EDGE ( 'NONE', *, *, #97905, .F. ) ;
#29378=AXIS2_PLACEMENT_3D ( 'NONE', #15086, #63125, #12956 ) ;
#29409=CARTESIAN_POINT ( 'NONE',  ( -1.098735407080257076, -7.248058225760418694, -6.326622577870835151 ) ) ;
#29440=ORIENTED_EDGE ( 'NONE', *, *, #2196, .F. ) ;
#29488=CARTESIAN_POINT ( 'NONE',  ( 0.000000000000000000, 0.000000000000000000, -6.800000000000000711 ) ) ;
#29520=CARTESIAN_POINT ( 'NONE',  ( 4.574783636564629496, 5.228990388887477359, -6.171384342982557669 ) ) ;
#29590=CARTESIAN_POINT ( 'NONE',  ( 0.000000000000000000, 0.000000000000000000, -8.000000000000000000 ) ) ;
#29612=CARTESIAN_POINT ( 'NONE',  ( -3.981862520314373377, 4.887481193368610871E-16, -0.01269999999999786924 ) ) ;
#29666=VERTEX_POINT ( 'NONE', #24789 ) ;
#29687=ORIENTED_EDGE ( 'NONE', *, *, #6332, .F. ) ;
#29839=CIRCLE ( 'NONE', #65920, 4.000000000000000000 ) ;
#29859=ORIENTED_EDGE ( 'NONE', *, *, #661, .F. ) ;
#29868=EDGE_CURVE ( 'NONE', #50026, #23499, #97784, .T. ) ;
#29911=EDGE_CURVE ( 'NONE', #28086, #84887, #68562, .T. ) ;
#29912=AXIS2_PLACEMENT_3D ( 'NONE', #79009, #78474, #6166 ) ;
#29923=CARTESIAN_POINT ( 'NONE',  ( -6.725979247667767780, -3.622307570260332454, -6.470294263593363127 ) ) ;
#29927=ADVANCED_FACE ( 'NONE', ( #54869 ), #46272, .F. ) ;
#29928=CARTESIAN_POINT ( 'NONE',  ( -5.589124336234561063, 4.278671059405865229, -6.219623095966342774 ) ) ;
#29959=FACE_OUTER_BOUND ( 'NONE', #53859, .T. ) ;
#29982=ORIENTED_EDGE ( 'NONE', *, *, #101587, .F. ) ;
#30015=ADVANCED_FACE ( 'NONE', ( #105037 ), #77089, .F. ) ;
#30031=CARTESIAN_POINT ( 'NONE',  ( 0.9108756637677339896, 6.979659189795291319, -6.219623095965904902 ) ) ;
#30035=CARTESIAN_POINT ( 'NONE',  ( -0.5620262070071395666, 7.564407249984303583, -6.443844059477449981 ) ) ;
#30146=FACE_OUTER_BOUND ( 'NONE', #98000, .T. ) ;
#30156=VERTEX_POINT ( 'NONE', #13092 ) ;
#30338=CARTESIAN_POINT ( 'NONE',  ( -2.352990130084491319E-16, 7.505553499465148271, -8.000000000000000000 ) ) ;
#30459=CARTESIAN_POINT ( 'NONE',  ( 0.04050535873994128011, 7.919512791578243949, -6.573129608219097086 ) ) ;
#30461=ADVANCED_FACE ( 'NONE', ( #12963 ), #97073, .F. ) ;
#30489=DIRECTION ( 'NONE',  ( 1.000000000000000000, 0.000000000000000000, 0.000000000000000000 ) ) ;
#30528=ADVANCED_FACE ( 'NONE', ( #56605 ), #51362, .F. ) ;
#30530=ORIENTED_EDGE ( 'NONE', *, *, #72817, .T. ) ;
#30644=AXIS2_PLACEMENT_3D ( 'NONE', #21412, #79607, #54791 ) ;
#30694=ORIENTED_EDGE ( 'NONE', *, *, #98938, .T. ) ;
#30706=EDGE_LOOP ( 'NONE', ( #21739, #47370, #91619, #48872 ) ) ;
#30848=AXIS2_PLACEMENT_3D ( 'NONE', #18558, #42805, #68702 ) ;
#30891=CONICAL_SURFACE ( 'NONE', #53271, 3.400000000000000355, 0.9599310885968748153 ) ;
#30947=CARTESIAN_POINT ( 'NONE',  ( -6.499999999999999112, 3.149025070564746898, -0.5705737632550961225 ) ) ;
#31175=AXIS2_PLACEMENT_3D ( 'NONE', #77085, #33460, #66334 ) ;
#31227=CARTESIAN_POINT ( 'NONE',  ( -3.250000000000002220, 5.629165124598849879, -5.592027715088708995 ) ) ;
#31349=DIRECTION ( 'NONE',  ( -1.000000000000000000, 0.000000000000000000, 0.000000000000000000 ) ) ;
#31424=EDGE_LOOP ( 'NONE', ( #71591, #101299, #56423, #14956 ) ) ;
#31429=VERTEX_POINT ( 'NONE', #66395 ) ;
#31462=AXIS2_PLACEMENT_3D ( 'NONE', #68488, #101377, #27530 ) ;
#31560=DIRECTION ( 'NONE',  ( -1.000000000000000000, 0.000000000000000000, 0.000000000000000000 ) ) ;
#31566=MECHANICAL_DESIGN_GEOMETRIC_PRESENTATION_REPRESENTATION('',(#33246),#84969);
#31589=EDGE_CURVE ( 'NONE', #41440, #5773, #6709, .T. ) ;
#31605=CARTESIAN_POINT ( 'NONE',  ( -6.837824896291513355, -3.947820044545450102, -6.564402953523720718 ) ) ;
#31611=EDGE_CURVE ( 'NONE', #27489, #100791, #101176, .T. ) ;
#31667=CARTESIAN_POINT ( 'NONE',  ( 0.000000000000000000, 0.000000000000000000, -4.987924522925830217 ) ) ;
#31725=LINE ( 'NONE', #91023, #78089 ) ;
#31741=CARTESIAN_POINT ( 'NONE',  ( -5.416666666666666075, 4.378239541354655984, -5.848636054922035754 ) ) ;
#31747=PLANE ( 'NONE',  #80807 ) ;
#31779=CARTESIAN_POINT ( 'NONE',  ( -3.250000000000016431, 5.629165124598842773, 1.734723475976807094E-15 ) ) ;
#31792=LINE ( 'NONE', #64677, #65557 ) ;
#31827=CARTESIAN_POINT ( 'NONE',  ( -6.837824896291514243, 3.947820044545419016, -6.564402953523714501 ) ) ;
#31834=DIRECTION ( 'NONE',  ( -1.000000000000000000, 0.000000000000000000, 0.000000000000000000 ) ) ;
#31862=CARTESIAN_POINT ( 'NONE',  ( 0.000000000000000000, 0.000000000000000000, -0.02540000000000007530 ) ) ;
#31869=EDGE_LOOP ( 'NONE', ( #2186, #24582, #82370, #18950 ) ) ;
#31881=CONICAL_SURFACE ( 'NONE', #92132, 3.400000000000000355, 0.9599310885968748153 ) ;
#31985=EDGE_CURVE ( 'NONE', #37787, #26262, #104891, .T. ) ;
#31994=EDGE_CURVE ( 'NONE', #14702, #112, #58374, .T. ) ;
#32057=CARTESIAN_POINT ( 'NONE',  ( 0.000000000000000000, 0.000000000000000000, -2.716724522925831220 ) ) ;
#32126=AXIS2_PLACEMENT_3D ( 'NONE', #38788, #86818, #103510 ) ;
#32204=ORIENTED_EDGE ( 'NONE', *, *, #97255, .T. ) ;
#32223=AXIS2_PLACEMENT_3D ( 'NONE', #63387, #95734, #56298 ) ;
#32230=AXIS2_PLACEMENT_3D ( 'NONE', #105461, #9394, #67667 ) ;
#32248=CARTESIAN_POINT ( 'NONE',  ( 0.000000000000000000, 0.000000000000000000, -3.432199999999999918 ) ) ;
#32269=CARTESIAN_POINT ( 'NONE',  ( -2.352990130084491319E-16, 7.505553499465148271, -6.064240316920404439 ) ) ;
#32318=CARTESIAN_POINT ( 'NONE',  ( 3.400000000000000355, 0.000000000000000000, -2.716724522925831220 ) ) ;
#32338=CARTESIAN_POINT ( 'NONE',  ( 6.499999999999999112, 3.752776749732559036, -6.064240316920397333 ) ) ;
#32481=AXIS2_PLACEMENT_3D ( 'NONE', #53169, #86620, #102239 ) ;
#32551=DIRECTION ( 'NONE',  ( -1.000000000000000000, 0.000000000000000000, 0.000000000000000000 ) ) ;
#32555=CLOSED_SHELL ( 'NONE', ( #62309, #88998, #21064, #15742, #104999, #4676, #30015, #104447, #98588, #1295, #88531, #12706, #106267, #57703, #39645, #91903, #80423, #57843, #96628, #99403, #98076, #97530, #30461, #97663, #15539, #51928, #29927, #35546, #85040, #32594, #74032, #88671, #73100, #83076, #105223, #103288, #57062, #90519, #66169, #45323, #75332, #71864, #4855, #85045, #11826, #20556, #73504, #57039, #51549, #54879, #80131, #101595, #68029, #104802, #74154, #46863, #52561, #52549, #24334, #28741, #83953, #62276, #97978, #61649, #3463, #43199, #35091, #64461, #30528, #40153, #11396, #52873 ) ) ;
#32594=ADVANCED_FACE ( 'NONE', ( #72261 ), #15611, .F. ) ;
#32614=VECTOR ( 'NONE', #76349, 1000.000000000000000 ) ;
#32663=FACE_OUTER_BOUND ( 'NONE', #48023, .T. ) ;
#32717=CARTESIAN_POINT ( 'NONE',  ( -0.04050535873994216135, -7.919512791578273259, -6.573129608219107745 ) ) ;
#32944=EDGE_CURVE ( 'NONE', #94655, #31429, #83950, .T. ) ;
#32952=CARTESIAN_POINT ( 'NONE',  ( 6.815765296784520366, 0.6502800852029971823, -6.170377922158429840 ) ) ;
#33005=CIRCLE ( 'NONE', #27884, 6.500000000000000000 ) ;
#33227=EDGE_CURVE ( 'NONE', #84887, #28086, #39450, .T. ) ;
#33241=CARTESIAN_POINT ( 'NONE',  ( 5.727634848076907481, -4.575561887447414655, -6.326622577870443465 ) ) ;
#33246=STYLED_ITEM ( 'NONE', ( #86013 ), #92356 ) ;
#33295=VECTOR ( 'NONE', #7711, 1000.000000000000000 ) ;
#33321=DIRECTION ( 'NONE',  ( -0.000000000000000000, -0.000000000000000000, -1.000000000000000000 ) ) ;
#33356=FACE_OUTER_BOUND ( 'NONE', #26176, .T. ) ;
#33460=DIRECTION ( 'NONE',  ( 0.000000000000000000, 0.000000000000000000, -1.000000000000000000 ) ) ;
#33573=EDGE_LOOP ( 'NONE', ( #30694, #38131, #59459, #14822 ) ) ;
#33597=DIRECTION ( 'NONE',  ( 1.000000000000000000, 0.000000000000000000, 0.000000000000000000 ) ) ;
#33606=CARTESIAN_POINT ( 'NONE',  ( -6.499999999999999112, -2.534234941938130703, -0.3584823952106149791 ) ) ;
#33626=CARTESIAN_POINT ( 'NONE',  ( 0.000000000000000000, 0.000000000000000000, -2.296599999999999753 ) ) ;
#33839=DIRECTION ( 'NONE',  ( 0.000000000000000000, 0.000000000000000000, 1.000000000000000000 ) ) ;
#33889=VECTOR ( 'NONE', #14489, 1000.000000000000114 ) ;
#33891=CARTESIAN_POINT ( 'NONE',  ( 0.000000000000000000, 0.000000000000000000, -5.703399999999999359 ) ) ;
#34174=B_SPLINE_CURVE_WITH_KNOTS ( 'NONE', 3,
 ( #47523, #97656, #70751, #14612, #103646 ),
 .UNSPECIFIED., .F., .F.,
 ( 4, 1, 4 ),
 ( 0.000000000000000000, 0.003752776749732572234, 0.007505553499465144468 ),
 .UNSPECIFIED. ) ;
#34260=CARTESIAN_POINT ( 'NONE',  ( -6.826580258811424606, 2.695816818219042954, -6.331007506862903256 ) ) ;
#34284=CARTESIAN_POINT ( 'NONE',  ( 0.000000000000000000, 0.000000000000000000, -3.852324522925831385 ) ) ;
#34305=AXIS2_PLACEMENT_3D ( 'NONE', #68778, #60686, #13153 ) ;
#34318=CARTESIAN_POINT ( 'NONE',  ( -6.499999999999999112, -3.752776749732587902, -6.064240316920403551 ) ) ;
#34388=DIRECTION ( 'NONE',  ( -0.000000000000000000, -0.000000000000000000, 1.000000000000000000 ) ) ;
#34480=ORIENTED_EDGE ( 'NONE', *, *, #96851, .T. ) ;
#34605=CARTESIAN_POINT ( 'NONE',  ( -6.826399921716642005, -2.638123634694639730, -6.344399053232586461 ) ) ;
#34694=FACE_OUTER_BOUND ( 'NONE', #97249, .T. ) ;
#34721=EDGE_LOOP ( 'NONE', ( #44509, #78743 ) ) ;
#34748=VERTEX_POINT ( 'NONE', #38028 ) ;
#34797=CARTESIAN_POINT ( 'NONE',  ( 6.499999999999999112, 3.752776749732595452, -0.7999999999999977129 ) ) ;
#34798=AXIS2_PLACEMENT_3D ( 'NONE', #21414, #36552, #11145 ) ;
#34936=EDGE_LOOP ( 'NONE', ( #89404, #10581, #83410, #61336 ) ) ;
#35020=EDGE_CURVE ( 'NONE', #102954, #94099, #45182, .T. ) ;
#35091=ADVANCED_FACE ( 'NONE', ( #55867 ), #66357, .F. ) ;
#35177=AXIS2_PLACEMENT_3D ( 'NONE', #43532, #42452, #59724 ) ;
#35230=DIRECTION ( 'NONE',  ( -1.000000000000000000, 0.000000000000000000, 0.000000000000000000 ) ) ;
#35238=EDGE_CURVE ( 'NONE', #26262, #37787, #14689, .T. ) ;
#35315=ORIENTED_EDGE ( 'NONE', *, *, #70678, .F. ) ;
#35319=CARTESIAN_POINT ( 'NONE',  ( 0.000000000000000000, 0.000000000000000000, -6.838999999999999524 ) ) ;
#35326=CARTESIAN_POINT ( 'NONE',  ( -6.838238953609875104, 3.993985489099926678, -6.572971244646267586 ) ) ;
#35363=VERTEX_POINT ( 'NONE', #81101 ) ;
#35454=ORIENTED_EDGE ( 'NONE', *, *, #32944, .T. ) ;
#35546=ADVANCED_FACE ( 'NONE', ( #60579 ), #2296, .F. ) ;
#35599=CONICAL_SURFACE ( 'NONE', #38955, 3.400000000000000355, 0.9599310885968748153 ) ;
#35690=CARTESIAN_POINT ( 'NONE',  ( 4.000000000000002665, 4.898587196589416773E-16, -7.974599999999995248 ) ) ;
#35716=CARTESIAN_POINT ( 'NONE',  ( 0.000000000000000000, 0.000000000000000000, -8.000000000000000000 ) ) ;
#35751=ORIENTED_EDGE ( 'NONE', *, *, #88011, .F. ) ;
#35841=CIRCLE ( 'NONE', #18656, 4.000000000000000000 ) ;
#35925=CARTESIAN_POINT ( 'NONE',  ( 5.007715329123895321E-16, -7.505553499465175804, -6.064240316920414209 ) ) ;
#35977=EDGE_CURVE ( 'NONE', #67283, #83820, #98222, .T. ) ;
#35991=FACE_OUTER_BOUND ( 'NONE', #102834, .T. ) ;
#36059=CIRCLE ( 'NONE', #53266, 6.500000000000000000 ) ;
#36079=B_SPLINE_CURVE_WITH_KNOTS ( 'NONE', 3,
 ( #3769, #10764, #94377, #92762, #3230, #85761, #69041, #18370 ),
 .UNSPECIFIED., .F., .F.,
 ( 4, 2, 2, 4 ),
 ( 2.459764730620682454E-07, 0.001920659145285692239, 0.002880865729692007153, 0.003841072314098320766 ),
 .UNSPECIFIED. ) ;
#36098=CARTESIAN_POINT ( 'NONE',  ( 3.400000000000000355, 0.000000000000000000, -3.852324522925831385 ) ) ;
#36099=ORIENTED_EDGE ( 'NONE', *, *, #80253, .T. ) ;
#36275=DIRECTION ( 'NONE',  ( 0.8191520442889974607, 1.003171929053531649E-16, -0.5735764363510379438 ) ) ;
#36281=CARTESIAN_POINT ( 'NONE',  ( 3.983107665916330475, -5.570601890521310828, -6.171481112545259329 ) ) ;
#36286=CARTESIAN_POINT ( 'NONE',  ( 0.000000000000000000, 0.000000000000000000, -0.7408754770741831086 ) ) ;
#36329=DIRECTION ( 'NONE',  ( 1.000000000000000000, 0.000000000000000000, 0.000000000000000000 ) ) ;
#36348=EDGE_LOOP ( 'NONE', ( #57973, #104660, #53300, #100453 ) ) ;
#36486=ORIENTED_EDGE ( 'NONE', *, *, #65954, .T. ) ;
#36493=ORIENTED_EDGE ( 'NONE', *, *, #100708, .T. ) ;
#36552=DIRECTION ( 'NONE',  ( 0.000000000000000000, 0.000000000000000000, 1.000000000000000000 ) ) ;
#36570=VECTOR ( 'NONE', #60814, 1000.000000000000000 ) ;
#36759=DIRECTION ( 'NONE',  ( 1.000000000000000000, 0.000000000000000000, 0.000000000000000000 ) ) ;
#36837=EDGE_CURVE ( 'NONE', #26529, #9488, #86837, .T. ) ;
#36887=EDGE_CURVE ( 'NONE', #70568, #25185, #54036, .T. ) ;
#36890=DIRECTION ( 'NONE',  ( 0.000000000000000000, 0.000000000000000000, 1.000000000000000000 ) ) ;
#36937=( NAMED_UNIT ( * ) PLANE_ANGLE_UNIT ( ) SI_UNIT ( $, .RADIAN. ) );
#36966=CARTESIAN_POINT ( 'NONE',  ( 0.04050535873993678371, -7.919512791578269706, -6.573129608219105968 ) ) ;
#36970=CARTESIAN_POINT ( 'NONE',  ( -4.444974277458379142, 4.939246403833572607, -5.720331885004773298 ) ) ;
#37037=CARTESIAN_POINT ( 'NONE',  ( -3.400000000000000355, 4.163799117101001052E-16, -3.852324522925831385 ) ) ;
#37076=CARTESIAN_POINT ( 'NONE',  ( 5.589124336234648993, 4.278671059403449384, -6.219623095964921689 ) ) ;
#37126=ORIENTED_EDGE ( 'NONE', *, *, #42643, .T. ) ;
#37149=VECTOR ( 'NONE', #48598, 1000.000000000000114 ) ;
#37224=EDGE_LOOP ( 'NONE', ( #39502, #74851, #76882, #91636 ) ) ;
#37236=CONICAL_SURFACE ( 'NONE', #50959, 4.000000000000000000, 0.9599310885968912466 ) ;
#37303=CONICAL_SURFACE ( 'NONE', #13142, 8.542937654374686218, 1.221730476396047704 ) ;
#37334=CARTESIAN_POINT ( 'NONE',  ( 2.263183130831067924, -6.566419505188308747, -6.208110906918269833 ) ) ;
#37427=VERTEX_POINT ( 'NONE', #6428 ) ;
#37451=CARTESIAN_POINT ( 'NONE',  ( -6.500000000000000000, 1.602771114417260501, -0.1495523863686117338 ) ) ;
#37508=CARTESIAN_POINT ( 'NONE',  ( -0.9108756637670308853, 6.979659189795754060, -6.219623095964492698 ) ) ;
#37518=DIRECTION ( 'NONE',  ( -1.000000000000000000, 0.000000000000000000, 0.000000000000000000 ) ) ;
#37530=VERTEX_POINT ( 'NONE', #70538 ) ;
#37556=VECTOR ( 'NONE', #26027, 1000.000000000000000 ) ;
#37674=CIRCLE ( 'NONE', #51391, 3.400000000000000355 ) ;
#37709=ORIENTED_EDGE ( 'NONE', *, *, #86157, .T. ) ;
#37771=AXIS2_PLACEMENT_3D ( 'NONE', #16843, #82632, #80487 ) ;
#37786=EDGE_LOOP ( 'NONE', ( #77873, #98403, #18681, #62074, #101212, #47815, #561 ) ) ;
#37787=VERTEX_POINT ( 'NONE', #40280 ) ;
#37945=( BOUNDED_SURFACE ( )  B_SPLINE_SURFACE ( 3, 2, ( 
 ( #62288, #29923, #22374 ),
 ( #14755, #95179, #21311 ),
 ( #55734, #70365, #69831 ),
 ( #62810, #87616, #77925 ),
 ( #54682, #21840, #29409 ),
 ( #12634, #54148, #36966 ) ),
 .UNSPECIFIED., .F., .F., .F. ) 
 B_SPLINE_SURFACE_WITH_KNOTS ( ( 4, 2, 4 ),
 ( 3, 3 ),
 ( 0.003190620565844245072, 0.007281897438794512727, 0.01137317431174478082 ),
 ( 0.000000000000000000, 1.000000000000000000 ),
 .UNSPECIFIED. ) 
 GEOMETRIC_REPRESENTATION_ITEM ( )  RATIONAL_B_SPLINE_SURFACE ( (
 ( 1.000000000000000000, 0.8047731410850402778, 1.000000000000000000),
 ( 1.000000000000000000, 0.8125552299157379199, 1.000000000000000000),
 ( 1.000000000000000000, 0.8191520442888340359, 1.000000000000000000),
 ( 1.000000000000000000, 0.8191520442891404574, 1.000000000000000000),
 ( 1.000000000000000000, 0.8125552299155076597, 1.000000000000000000),
 ( 1.000000000000000000, 0.8047731410850398337, 1.000000000000000000) ) ) 
 REPRESENTATION_ITEM ( '' )  SURFACE ( )  );
#37966=DIRECTION ( 'NONE',  ( 0.000000000000000000, 0.000000000000000000, 1.000000000000000000 ) ) ;
#37984=CARTESIAN_POINT ( 'NONE',  ( -6.500000000000000000, 0.3213925021621101830, 3.146515640812911001E-15 ) ) ;
#38000=VERTEX_POINT ( 'NONE', #84867 ) ;
#38006=CARTESIAN_POINT ( 'NONE',  ( -6.500000000000002665, -2.501851166488398892, -5.848636054922038419 ) ) ;
#38028=CARTESIAN_POINT ( 'NONE',  ( 3.400000000000000355, 0.000000000000000000, -0.7408754770741831086 ) ) ;
#38034=CARTESIAN_POINT ( 'NONE',  ( 0.2259792476677729700, 7.636022678937404606, -6.470294263593366679 ) ) ;
#38108=DIRECTION ( 'NONE',  ( -0.000000000000000000, -0.000000000000000000, 1.000000000000000000 ) ) ;
#38131=ORIENTED_EDGE ( 'NONE', *, *, #47726, .T. ) ;
#38149=VECTOR ( 'NONE', #103334, 1000.000000000000000 ) ;
#38150=CARTESIAN_POINT ( 'NONE',  ( -3.250000000000013767, -5.629165124598844550, 1.734723475976807094E-15 ) ) ;
#38167=DIRECTION ( 'NONE',  ( -0.000000000000000000, -0.000000000000000000, -1.000000000000000000 ) ) ;
#38241=CARTESIAN_POINT ( 'NONE',  ( 0.000000000000000000, 0.000000000000000000, -8.000000000000000000 ) ) ;
#38260=CARTESIAN_POINT ( 'NONE',  ( -8.542937654374686218, 0.000000000000000000, -6.800000000000000711 ) ) ;
#38495=CARTESIAN_POINT ( 'NONE',  ( -6.500000000000000000, 2.536640449112266271, -0.3753468889000121100 ) ) ;
#38546=DIRECTION ( 'NONE',  ( -0.000000000000000000, -0.000000000000000000, -1.000000000000000000 ) ) ;
#38555=EDGE_CURVE ( 'NONE', #82973, #88610, #35841, .T. ) ;
#38639=AXIS2_PLACEMENT_3D ( 'NONE', #78540, #94208, #62907 ) ;
#38659=LINE ( 'NONE', #96879, #100265 ) ;
#38670=CARTESIAN_POINT ( 'NONE',  ( 0.000000000000000000, 0.000000000000000000, -3.432199999999999918 ) ) ;
#38672=B_SPLINE_CURVE_WITH_KNOTS ( 'NONE', 3,
 ( #61053, #102565, #85873, #12998, #68622, #27119 ),
 .UNSPECIFIED., .F., .F.,
 ( 4, 2, 4 ),
 ( 0.003981881017442815036, 0.005970145066490141136, 0.007958409115537466369 ),
 .UNSPECIFIED. ) ;
#38689=CYLINDRICAL_SURFACE ( 'NONE', #57572, 3.400000000000000355 ) ;
#38788=CARTESIAN_POINT ( 'NONE',  ( 0.000000000000000000, 0.000000000000000000, -0.01269999999999786924 ) ) ;
#38803=EDGE_CURVE ( 'NONE', #102690, #18921, #68528, .T. ) ;
#38812=VECTOR ( 'NONE', #53261, 1000.000000000000114 ) ;
#38842=ORIENTED_EDGE ( 'NONE', *, *, #100402, .T. ) ;
#38846=CARTESIAN_POINT ( 'NONE',  ( -4.000000000000000000, 0.000000000000000000, -3.432199999999999918 ) ) ;
#38911=CARTESIAN_POINT ( 'NONE',  ( 6.499999999999998224, 0.6659426636834143709, -5.719325464431598505 ) ) ;
#38955=AXIS2_PLACEMENT_3D ( 'NONE', #97066, #36890, #84874 ) ;
#38997=FACE_OUTER_BOUND ( 'NONE', #34936, .T. ) ;
#38999=DIRECTION ( 'NONE',  ( -1.000000000000000000, 0.000000000000000000, 0.000000000000000000 ) ) ;
#39067=EDGE_CURVE ( 'NONE', #73863, #94099, #62776, .T. ) ;
#39180=CARTESIAN_POINT ( 'NONE',  ( -2.837346585668845567, 6.232092946297383307, -6.171287963165197787 ) ) ;
#39231=ORIENTED_EDGE ( 'NONE', *, *, #40212, .T. ) ;
#39365=CARTESIAN_POINT ( 'NONE',  ( 2.262848203703084149, 6.566616684922156999, -6.208169345099793901 ) ) ;
#39396=CARTESIAN_POINT ( 'NONE',  ( 0.000000000000000000, 0.000000000000000000, -8.000000000000000000 ) ) ;
#39446=CARTESIAN_POINT ( 'NONE',  ( 6.499999999999998224, 3.350125858420228919, -6.343571411522940018 ) ) ;
#39450=CIRCLE ( 'NONE', #37771, 4.000000000000002665 ) ;
#39502=ORIENTED_EDGE ( 'NONE', *, *, #5543, .F. ) ;
#39542=ORIENTED_EDGE ( 'NONE', *, *, #39683, .T. ) ;
#39573=ORIENTED_EDGE ( 'NONE', *, *, #65954, .F. ) ;
#39574=SHAPE_REPRESENTATION_RELATIONSHIP ( 'NONE' , 'NONE' ,  #25516, #92356 ) ;
#39588=DIRECTION ( 'NONE',  ( -0.000000000000000000, -0.000000000000000000, -1.000000000000000000 ) ) ;
#39645=ADVANCED_FACE ( 'NONE', ( #51203 ), #75491, .F. ) ;
#39660=LINE ( 'NONE', #47717, #1830 ) ;
#39683=EDGE_CURVE ( 'NONE', #717, #27489, #84125, .T. ) ;
#39714=DIRECTION ( 'NONE',  ( -0.8191520442889974607, 0.000000000000000000, -0.5735764363510379438 ) ) ;
#39722=PRODUCT_DEFINITION ( 'UNKNOWN', '', #6022, #68291 ) ;
#39724=APPLICATION_CONTEXT ( 'automotive_design' ) ;
#39907=DIRECTION ( 'NONE',  ( -1.000000000000000000, 0.000000000000000000, 0.000000000000000000 ) ) ;
#39963=CARTESIAN_POINT ( 'NONE',  ( 6.499999999999999112, 4.077976443323001909, -6.122137821720841977 ) ) ;
#39974=DIRECTION ( 'NONE',  ( -0.8191520442889974607, 0.000000000000000000, -0.5735764363510379438 ) ) ;
#39992=DIRECTION ( 'NONE',  ( -1.000000000000000000, 0.000000000000000000, 0.000000000000000000 ) ) ;
#39998=VERTEX_POINT ( 'NONE', #93710 ) ;
#40090=CARTESIAN_POINT ( 'NONE',  ( -6.499999999999999112, -1.604619215278546562E-14, -5.592027715088706330 ) ) ;
#40097=CARTESIAN_POINT ( 'NONE',  ( -3.220999722221654600E-16, 7.895640089090876224, -6.564402953523721607 ) ) ;
#40100=CARTESIAN_POINT ( 'NONE',  ( 3.400000000000000355, 0.000000000000000000, -8.000000000000000000 ) ) ;
#40151=DIRECTION ( 'NONE',  ( -1.000000000000000000, 0.000000000000000000, 0.000000000000000000 ) ) ;
#40153=ADVANCED_FACE ( 'NONE', ( #58954 ), #30891, .F. ) ;
#40170=DIRECTION ( 'NONE',  ( 0.000000000000000000, 0.000000000000000000, -1.000000000000000000 ) ) ;
#40199=DIRECTION ( 'NONE',  ( 1.000000000000000000, 0.000000000000000000, 0.000000000000000000 ) ) ;
#40212=EDGE_CURVE ( 'NONE', #62903, #102355, #6767, .T. ) ;
#40280=CARTESIAN_POINT ( 'NONE',  ( 3.400000000000000355, 0.000000000000000000, -3.012075477074183105 ) ) ;
#40310=ORIENTED_EDGE ( 'NONE', *, *, #10494, .T. ) ;
#40324=DIRECTION ( 'NONE',  ( 0.000000000000000000, 0.000000000000000000, 1.000000000000000000 ) ) ;
#40398=CARTESIAN_POINT ( 'NONE',  ( 6.499999999999999112, -1.431146867680865853E-14, -5.592027715088708106 ) ) ;
#40500=LINE ( 'NONE', #16215, #51543 ) ;
#40563=ORIENTED_EDGE ( 'NONE', *, *, #47774, .F. ) ;
#40596=VERTEX_POINT ( 'NONE', #20005 ) ;
#40705=LINE ( 'NONE', #73593, #5733 ) ;
#40853=CARTESIAN_POINT ( 'NONE',  ( 0.000000000000000000, 0.000000000000000000, -2.296599999999999753 ) ) ;
#40890=DIRECTION ( 'NONE',  ( 0.000000000000000000, 0.000000000000000000, 1.000000000000000000 ) ) ;
#41020=CARTESIAN_POINT ( 'NONE',  ( 6.499999999999999112, -2.759515168581767153, -5.880113447610368027 ) ) ;
#41159=CARTESIAN_POINT ( 'NONE',  ( 2.141486166123602430, -6.269165884987846660, -0.07763482564822672682 ) ) ;
#41253=ORIENTED_EDGE ( 'NONE', *, *, #50111, .T. ) ;
#41295=CARTESIAN_POINT ( 'NONE',  ( 6.499999999999999112, -3.752776749732586126, -6.064240316920402663 ) ) ;
#41324=FACE_OUTER_BOUND ( 'NONE', #3973, .T. ) ;
#41381=VECTOR ( 'NONE', #99993, 1000.000000000000000 ) ;
#41389=LINE ( 'NONE', #97481, #11425 ) ;
#41414=DIRECTION ( 'NONE',  ( -0.000000000000000000, -0.000000000000000000, -1.000000000000000000 ) ) ;
#41416=EDGE_CURVE ( 'NONE', #87758, #15859, #93850, .T. ) ;
#41434=VECTOR ( 'NONE', #103346, 1000.000000000000000 ) ;
#41440=VERTEX_POINT ( 'NONE', #49548 ) ;
#41481=CARTESIAN_POINT ( 'NONE',  ( 1.960217980381542535E-15, -7.550815748621879209, -6.286450516131066202 ) ) ;
#41751=ORIENTED_EDGE ( 'NONE', *, *, #22779, .F. ) ;
#41773=ORIENTED_EDGE ( 'NONE', *, *, #41416, .F. ) ;
#41863=LINE ( 'NONE', #830, #93134 ) ;
#42183=AXIS2_PLACEMENT_3D ( 'NONE', #32057, #82164, #99396 ) ;
#42199=FACE_OUTER_BOUND ( 'NONE', #9813, .T. ) ;
#42219=DIRECTION ( 'NONE',  ( -0.000000000000000000, -0.000000000000000000, -1.000000000000000000 ) ) ;
#42311=CARTESIAN_POINT ( 'NONE',  ( -6.815701034932152957, -1.328907527193361693, -6.169383458210041304 ) ) ;
#42349=EDGE_CURVE ( 'NONE', #25389, #37427, #106334, .T. ) ;
#42452=DIRECTION ( 'NONE',  ( 0.000000000000000000, 0.000000000000000000, 1.000000000000000000 ) ) ;
#42469=CARTESIAN_POINT ( 'NONE',  ( -2.690931834596291594, 5.951943280390036506, 1.837214462594576647E-15 ) ) ;
#42510=LINE ( 'NONE', #67857, #100924 ) ;
#42642=CARTESIAN_POINT ( 'NONE',  ( 0.000000000000000000, 0.000000000000000000, -25.03750572909317285 ) ) ;
#42643=EDGE_CURVE ( 'NONE', #88814, #30156, #11780, .T. ) ;
#42651=DIRECTION ( 'NONE',  ( 0.8191520442889881348, 0.000000000000000000, 0.5735764363510513775 ) ) ;
#42656=DIRECTION ( 'NONE',  ( 1.000000000000000000, 0.000000000000000000, 0.000000000000000000 ) ) ;
#42733=DIRECTION ( 'NONE',  ( 0.000000000000000000, 0.000000000000000000, 1.000000000000000000 ) ) ;
#42740=CARTESIAN_POINT ( 'NONE',  ( -6.500000000000000000, -0.6456425506958787253, 3.045930478326464019E-15 ) ) ;
#42800=PLANE ( 'NONE',  #66512 ) ;
#42805=DIRECTION ( 'NONE',  ( -0.000000000000000000, -0.000000000000000000, -1.000000000000000000 ) ) ;
#42850=CARTESIAN_POINT ( 'NONE',  ( 6.499999999999999112, 3.149025070564777984, -0.5705737632551077798 ) ) ;
#43093=DIRECTION ( 'NONE',  ( 1.000000000000000000, 0.000000000000000000, 0.000000000000000000 ) ) ;
#43104=EDGE_LOOP ( 'NONE', ( #100068, #68128, #54284, #69224 ) ) ;
#43199=ADVANCED_FACE ( 'NONE', ( #2947 ), #23922, .F. ) ;
#43345=DIRECTION ( 'NONE',  ( -1.000000000000000000, 0.000000000000000000, 0.000000000000000000 ) ) ;
#43526=CARTESIAN_POINT ( 'NONE',  ( -6.499999999999999112, 3.752776749732556816, -8.000000000000000000 ) ) ;
#43532=CARTESIAN_POINT ( 'NONE',  ( 0.000000000000000000, 0.000000000000000000, -8.000000000000000000 ) ) ;
#43551=LINE ( 'NONE', #69435, #36570 ) ;
#43576=CARTESIAN_POINT ( 'NONE',  ( 4.000000000000002665, 4.898587196589416773E-16, -7.974599999999995248 ) ) ;
#43588=CARTESIAN_POINT ( 'NONE',  ( 6.500000000000007105, -3.752776749732581685, -0.7999999999999977129 ) ) ;
#43648=DIRECTION ( 'NONE',  ( -0.8191520442889974607, 0.000000000000000000, -0.5735764363510379438 ) ) ;
#43734=DIRECTION ( 'NONE',  ( 0.8191520442889924647, 1.003171929053525486E-16, -0.5735764363510451602 ) ) ;
#43858=CARTESIAN_POINT ( 'NONE',  ( -4.466912950640278268E-14, -7.505553499465147382, -0.7999999999999977129 ) ) ;
#43915=CARTESIAN_POINT ( 'NONE',  ( -6.499999999999999112, 2.759383090079003065, -5.880088986489996117 ) ) ;
#43954=PLANE ( 'NONE',  #75397 ) ;
#43963=CIRCLE ( 'NONE', #28522, 3.400000000000000355 ) ;
#44002=AXIS2_PLACEMENT_3D ( 'NONE', #51359, #102039, #4412 ) ;
#44034=EDGE_CURVE ( 'NONE', #17532, #9879, #80947, .T. ) ;
#44134=B_SPLINE_CURVE_WITH_KNOTS ( 'NONE', 3,
 ( #76634, #11355, #100382, #44285, #28135, #2204 ),
 .UNSPECIFIED., .F., .F.,
 ( 4, 2, 4 ),
 ( -4.604908131561810387E-06, 0.0003318387708518404111, 0.0006682824498352427003 ),
 .UNSPECIFIED. ) ;
#44197=CIRCLE ( 'NONE', #23517, 8.542937654374686218 ) ;
#44198=FACE_OUTER_BOUND ( 'NONE', #59668, .T. ) ;
#44285=CARTESIAN_POINT ( 'NONE',  ( -6.539196172010133701, 3.775406670193810932, -6.286444963328660762 ) ) ;
#44359=DIRECTION ( 'NONE',  ( -1.000000000000000000, 0.000000000000000000, 0.000000000000000000 ) ) ;
#44469=( NAMED_UNIT ( * ) SI_UNIT ( $, .STERADIAN. ) SOLID_ANGLE_UNIT ( ) );
#44509=ORIENTED_EDGE ( 'NONE', *, *, #53562, .F. ) ;
#44518=DIRECTION ( 'NONE',  ( -0.000000000000000000, -0.000000000000000000, -1.000000000000000000 ) ) ;
#44539=LINE ( 'NONE', #45077, #51208 ) ;
#44603=FACE_OUTER_BOUND ( 'NONE', #51405, .T. ) ;
#44653=ORIENTED_EDGE ( 'NONE', *, *, #90096, .T. ) ;
#44691=B_SPLINE_CURVE_WITH_KNOTS ( 'NONE', 3,
 ( #34318, #99533, #27837, #26765, #35925 ),
 .UNSPECIFIED., .F., .F.,
 ( 4, 1, 4 ),
 ( 0.000000000000000000, 0.003752776749732571800, 0.007505553499465145335 ),
 .UNSPECIFIED. ) ;
#44711=CIRCLE ( 'NONE', #27496, 3.400000000000000355 ) ;
#44751=B_SPLINE_CURVE_WITH_KNOTS ( 'NONE', 3,
 ( #95654, #37984, #21268, #55684, #37451, #45523, #38495, #30947, #78396, #21791 ),
 .UNSPECIFIED., .F., .F.,
 ( 4, 2, 2, 2, 4 ),
 ( 0.009353627468483456664, 0.01031000219096074762, 0.01126637691343803857, 0.01222275163591532779, 0.01317912635839261874 ),
 .UNSPECIFIED. ) ;
#44752=CIRCLE ( 'NONE', #67067, 4.000000000000000888 ) ;
#45037=FACE_OUTER_BOUND ( 'NONE', #34721, .T. ) ;
#45070=DIRECTION ( 'NONE',  ( 0.000000000000000000, 0.000000000000000000, 1.000000000000000000 ) ) ;
#45077=CARTESIAN_POINT ( 'NONE',  ( 3.400000000000000355, 0.000000000000000000, -1.581124522925831499 ) ) ;
#45148=DIRECTION ( 'NONE',  ( -0.000000000000000000, -0.000000000000000000, 1.000000000000000000 ) ) ;
#45182=LINE ( 'NONE', #69451, #38812 ) ;
#45201=ORIENTED_EDGE ( 'NONE', *, *, #35238, .F. ) ;
#45237=ORIENTED_EDGE ( 'NONE', *, *, #75666, .F. ) ;
#45305=AXIS2_PLACEMENT_3D ( 'NONE', #3850, #2769, #60511 ) ;
#45323=ADVANCED_FACE ( 'NONE', ( #102882, #13848 ), #21454, .T. ) ;
#45333=AXIS2_PLACEMENT_3D ( 'NONE', #49476, #80782, #105590 ) ;
#45456=CARTESIAN_POINT ( 'NONE',  ( -1.127757440534757460, -7.231345287187126658, -6.344532336093720026 ) ) ;
#45523=CARTESIAN_POINT ( 'NONE',  ( -6.499999999999999112, 2.227636940139120725, -0.2900584647821155548 ) ) ;
#45535=CONICAL_SURFACE ( 'NONE', #76527, 6.500000000000000888, 0.8987552595851637793 ) ;
#45537=DIRECTION ( 'NONE',  ( -0.8191520442889881348, 1.003171929053520186E-16, 0.5735764363510513775 ) ) ;
#45609=EDGE_CURVE ( 'NONE', #17654, #104748, #44752, .T. ) ;
#45616=DIRECTION ( 'NONE',  ( -0.8191520442889881348, 1.003171929053520186E-16, 0.5735764363510513775 ) ) ;
#45691=ORIENTED_EDGE ( 'NONE', *, *, #76195, .F. ) ;
#45734=VECTOR ( 'NONE', #53051, 1000.000000000000000 ) ;
#45820=ORIENTED_EDGE ( 'NONE', *, *, #105012, .T. ) ;
#45901=VECTOR ( 'NONE', #70792, 1000.000000000000114 ) ;
#46026=CARTESIAN_POINT ( 'NONE',  ( 0.000000000000000000, 0.000000000000000000, -1.581124522925831499 ) ) ;
#46063=SURFACE_STYLE_FILL_AREA ( #52540 ) ;
#46091=FACE_OUTER_BOUND ( 'NONE', #21922, .T. ) ;
#46212=CARTESIAN_POINT ( 'NONE',  ( 0.000000000000000000, 0.000000000000000000, -5.703399999999999359 ) ) ;
#46272=CYLINDRICAL_SURFACE ( 'NONE', #11637, 3.400000000000000355 ) ;
#46310=ORIENTED_EDGE ( 'NONE', *, *, #90182, .F. ) ;
#46370=CARTESIAN_POINT ( 'NONE',  ( 6.746887896523637629, 3.895317543247282188, -6.526184258131186411 ) ) ;
#46371=ORIENTED_EDGE ( 'NONE', *, *, #15941, .T. ) ;
#46397=ORIENTED_EDGE ( 'NONE', *, *, #16456, .F. ) ;
#46401=LINE ( 'NONE', #38846, #69776 ) ;
#46470=DIRECTION ( 'NONE',  ( -1.000000000000000000, 0.000000000000000000, 0.000000000000000000 ) ) ;
#46680=CARTESIAN_POINT ( 'NONE',  ( 6.500000000000000888, 0.000000000000000000, 1.734723475976807094E-15 ) ) ;
#46690=CARTESIAN_POINT ( 'NONE',  ( 0.000000000000000000, 0.000000000000000000, -6.838999999999999524 ) ) ;
#46762=FACE_OUTER_BOUND ( 'NONE', #91341, .T. ) ;
#46794=DIRECTION ( 'NONE',  ( -0.000000000000000000, -0.000000000000000000, 1.000000000000000000 ) ) ;
#46862=CARTESIAN_POINT ( 'NONE',  ( 0.000000000000000000, 0.000000000000000000, -6.800000000000000711 ) ) ;
#46863=ADVANCED_FACE ( 'NONE', ( #87412 ), #100004, .F. ) ;
#46925=VERTEX_POINT ( 'NONE', #13486 ) ;
#46985=EDGE_CURVE ( 'NONE', #10770, #17481, #26551, .T. ) ;
#46994=DIRECTION ( 'NONE',  ( -0.000000000000000000, -0.000000000000000000, 1.000000000000000000 ) ) ;
#47136=CARTESIAN_POINT ( 'NONE',  ( -5.619193549420574918, 4.261310591078547816, -5.875704392895148231 ) ) ;
#47370=ORIENTED_EDGE ( 'NONE', *, *, #67267, .T. ) ;
#47380=CARTESIAN_POINT ( 'NONE',  ( 0.000000000000000000, 0.000000000000000000, 0.000000000000000000 ) ) ;
#47482=LINE ( 'NONE', #73884, #97122 ) ;
#47506=CARTESIAN_POINT ( 'NONE',  ( 6.499999999999999112, 4.014041399406593769, -6.470356572124274841 ) ) ;
#47523=CARTESIAN_POINT ( 'NONE',  ( 6.499999999999999112, 3.752776749732559036, -6.064240316920397333 ) ) ;
#47648=( BOUNDED_SURFACE ( )  B_SPLINE_SURFACE ( 3, 2, ( 
 ( #80936, #105746, #81988 ),
 ( #41020, #7566, #65821 ),
 ( #48026, #73901, #61188 ),
 ( #38911, #7047, #32952 ),
 ( #63724, #96609, #15145 ),
 ( #73362, #98184, #14594 ),
 ( #106261, #39446, #105226 ),
 ( #39963, #47506, #80399 ) ),
 .UNSPECIFIED., .F., .F., .F. ) 
 B_SPLINE_SURFACE_WITH_KNOTS ( ( 4, 2, 2, 4 ),
 ( 3, 3 ),
 ( 0.03170918191602133118, 0.03570420671717101924, 0.03770171911774586326, 0.03969923151832070035 ),
 ( 0.000000000000000000, 1.000000000000000000 ),
 .UNSPECIFIED. ) 
 GEOMETRIC_REPRESENTATION_ITEM ( )  RATIONAL_B_SPLINE_SURFACE ( (
 ( 1.000000000000000000, 0.8047781070930545289, 1.000000000000000000),
 ( 1.000000000000000000, 0.8123787894255036779, 1.000000000000000000),
 ( 1.000000000000000000, 0.8190667557155233425, 1.000000000000000000),
 ( 1.000000000000000000, 0.8191933945820393248, 1.000000000000000000),
 ( 1.000000000000000000, 0.8176087340367195200, 1.000000000000000000),
 ( 1.000000000000000000, 0.8122956952721525070, 1.000000000000000000),
 ( 1.000000000000000000, 0.8086308540101730946, 1.000000000000000000),
 ( 1.000000000000000000, 0.8047712493762132491, 1.000000000000000000) ) ) 
 REPRESENTATION_ITEM ( '' )  SURFACE ( )  );
#47717=CARTESIAN_POINT ( 'NONE',  ( 4.000000000000000000, 4.898587196589412829E-16, -3.432199999999999918 ) ) ;
#47726=EDGE_CURVE ( 'NONE', #31429, #62903, #104376, .T. ) ;
#47774=EDGE_CURVE ( 'NONE', #56514, #102690, #49390, .T. ) ;
#47776=DIRECTION ( 'NONE',  ( 1.000000000000000000, 0.000000000000000000, 0.000000000000000000 ) ) ;
#47815=ORIENTED_EDGE ( 'NONE', *, *, #96032, .T. ) ;
#47878=DIRECTION ( 'NONE',  ( 1.000000000000000000, 0.000000000000000000, 0.000000000000000000 ) ) ;
#47924=CARTESIAN_POINT ( 'NONE',  ( -4.639619758716991171, 4.826867782832367837, -0.1499059597315244019 ) ) ;
#47970=CARTESIAN_POINT ( 'NONE',  ( 0.000000000000000000, 0.000000000000000000, -7.259124522925831435 ) ) ;
#47975=ORIENTED_EDGE ( 'NONE', *, *, #2619, .F. ) ;
#48023=EDGE_LOOP ( 'NONE', ( #18002, #61084, #28910, #48775 ) ) ;
#48026=CARTESIAN_POINT ( 'NONE',  ( 6.499999999999998224, -1.417018949932255412, -5.722407714415304270 ) ) ;
#48128=EDGE_CURVE ( 'NONE', #14310, #73863, #25460, .T. ) ;
#48229=DIRECTION ( 'NONE',  ( -0.000000000000000000, -0.000000000000000000, 1.000000000000000000 ) ) ;
#48247=FACE_OUTER_BOUND ( 'NONE', #2382, .T. ) ;
#48280=DIRECTION ( 'NONE',  ( -1.000000000000000000, 0.000000000000000000, 0.000000000000000000 ) ) ;
#48349=DIRECTION ( 'NONE',  ( 0.8191520442889881348, 0.000000000000000000, 0.5735764363510513775 ) ) ;
#48352=CARTESIAN_POINT ( 'NONE',  ( 0.000000000000000000, 0.000000000000000000, 1.734723475976807094E-15 ) ) ;
#48431=CARTESIAN_POINT ( 'NONE',  ( 3.400000000000000355, 0.000000000000000000, -4.987924522925830217 ) ) ;
#48498=VECTOR ( 'NONE', #43648, 1000.000000000000114 ) ;
#48598=DIRECTION ( 'NONE',  ( 0.8191520442889974607, 1.003171929053531649E-16, -0.5735764363510379438 ) ) ;
#48619=VERTEX_POINT ( 'NONE', #36098 ) ;
#48672=ORIENTED_EDGE ( 'NONE', *, *, #52977, .T. ) ;
#48767=CARTESIAN_POINT ( 'NONE',  ( 3.400000000000000355, 0.000000000000000000, -7.259124522925831435 ) ) ;
#48775=ORIENTED_EDGE ( 'NONE', *, *, #81840, .F. ) ;
#48807=CIRCLE ( 'NONE', #29912, 3.400000000000000355 ) ;
#48872=ORIENTED_EDGE ( 'NONE', *, *, #33227, .T. ) ;
#48901=ORIENTED_EDGE ( 'NONE', *, *, #60962, .F. ) ;
#49155=CARTESIAN_POINT ( 'NONE',  ( -4.000000000000001776, 4.898587196589415787E-16, -8.000000000000000000 ) ) ;
#49339=VECTOR ( 'NONE', #87466, 1000.000000000000114 ) ;
#49387=ORIENTED_EDGE ( 'NONE', *, *, #42349, .T. ) ;
#49390=B_SPLINE_CURVE_WITH_KNOTS ( 'NONE', 3,
 ( #55286, #70958, #21909, #94184, #6204, #46680 ),
 .UNSPECIFIED., .F., .F.,
 ( 4, 2, 4 ),
 ( 0.005511122051665473358, 0.007432374760074465445, 0.009353627468483458399 ),
 .UNSPECIFIED. ) ;
#49415=AXIS2_PLACEMENT_3D ( 'NONE', #95577, #103660, #4975 ) ;
#49466=DIRECTION ( 'NONE',  ( 0.000000000000000000, 0.000000000000000000, 1.000000000000000000 ) ) ;
#49476=CARTESIAN_POINT ( 'NONE',  ( 0.000000000000000000, 0.000000000000000000, -0.01269999999999786924 ) ) ;
#49490=FACE_OUTER_BOUND ( 'NONE', #101354, .T. ) ;
#49548=CARTESIAN_POINT ( 'NONE',  ( -8.331345277524542681, 1.033251829022860324E-15, -8.000000000000000000 ) ) ;
#49670=EDGE_CURVE ( 'NONE', #3656, #74698, #27634, .T. ) ;
#49698=EDGE_CURVE ( 'NONE', #13321, #73863, #70829, .T. ) ;
#49723=AXIS2_PLACEMENT_3D ( 'NONE', #1038, #45148, #25939 ) ;
#49793=CARTESIAN_POINT ( 'NONE',  ( -3.220999722221654600E-16, 7.895640089090876224, -6.564402953523721607 ) ) ;
#49803=AXIS2_PLACEMENT_3D ( 'NONE', #12787, #20427, #95322 ) ;
#49857=EDGE_CURVE ( 'NONE', #40596, #71589, #1765, .T. ) ;
#50026=VERTEX_POINT ( 'NONE', #83963 ) ;
#50082=B_SPLINE_CURVE_WITH_KNOTS ( 'NONE', 3,
 ( #91308, #26079, #33606, #92342, #42740, #1734 ),
 .UNSPECIFIED., .F., .F.,
 ( 4, 2, 4 ),
 ( 0.005511122051665461215, 0.007432374760074458506, 0.009353627468483456664 ),
 .UNSPECIFIED. ) ;
#50111=EDGE_CURVE ( 'NONE', #72013, #64557, #20890, .T. ) ;
#50158=CARTESIAN_POINT ( 'NONE',  ( 0.000000000000000000, 0.000000000000000000, -2.716724522925831220 ) ) ;
#50230=CARTESIAN_POINT ( 'NONE',  ( -6.499999999999999112, -3.752776749732595452, -0.7999999999999977129 ) ) ;
#50281=CIRCLE ( 'NONE', #77863, 3.400000000000000355 ) ;
#50312=ORIENTED_EDGE ( 'NONE', *, *, #86149, .T. ) ;
#50392=CARTESIAN_POINT ( 'NONE',  ( 6.499999999999999112, 2.227636940139142929, -0.2900584647821211615 ) ) ;
#50465=FACE_OUTER_BOUND ( 'NONE', #37786, .T. ) ;
#50502=DIRECTION ( 'NONE',  ( 0.8191520442889900222, 0.000000000000000000, 0.5735764363510486019 ) ) ;
#50547=CARTESIAN_POINT ( 'NONE',  ( -0.5219667817988858927, 7.204195837485517728, -0.5602453477493318790 ) ) ;
#50585=ORIENTED_EDGE ( 'NONE', *, *, #55931, .F. ) ;
#50639=ORIENTED_EDGE ( 'NONE', *, *, #95545, .F. ) ;
#50763=CARTESIAN_POINT ( 'NONE',  ( -6.837824896291513355, -3.947820044545450102, -6.564402953523720718 ) ) ;
#50808=DIRECTION ( 'NONE',  ( 0.000000000000000000, 0.000000000000000000, -1.000000000000000000 ) ) ;
#50959=AXIS2_PLACEMENT_3D ( 'NONE', #54911, #87838, #72695 ) ;
#51022=CONICAL_SURFACE ( 'NONE', #91120, 4.000000000000000000, 0.9599310885968912466 ) ;
#51183=CIRCLE ( 'NONE', #96022, 4.000000000000000000 ) ;
#51189=ORIENTED_EDGE ( 'NONE', *, *, #91480, .T. ) ;
#51196=EDGE_CURVE ( 'NONE', #70568, #72013, #97907, .T. ) ;
#51203=FACE_OUTER_BOUND ( 'NONE', #31869, .T. ) ;
#51208=VECTOR ( 'NONE', #42651, 1000.000000000000000 ) ;
#51247=EDGE_LOOP ( 'NONE', ( #41751, #102433, #20463, #20478 ) ) ;
#51359=CARTESIAN_POINT ( 'NONE',  ( 0.000000000000000000, 0.000000000000000000, -8.000000000000000000 ) ) ;
#51362=CONICAL_SURFACE ( 'NONE', #94432, 4.000000000000000000, 0.9599310885968912466 ) ;
#51391=AXIS2_PLACEMENT_3D ( 'NONE', #15345, #48229, #40151 ) ;
#51405=EDGE_LOOP ( 'NONE', ( #54891, #34480, #105224, #19473 ) ) ;
#51409=ORIENTED_EDGE ( 'NONE', *, *, #35020, .T. ) ;
#51508=VECTOR ( 'NONE', #33839, 1000.000000000000000 ) ;
#51543=VECTOR ( 'NONE', #57725, 1000.000000000000000 ) ;
#51549=ADVANCED_FACE ( 'NONE', ( #42199 ), #76153, .T. ) ;
#51729=ORIENTED_EDGE ( 'NONE', *, *, #11356, .F. ) ;
#51790=FACE_OUTER_BOUND ( 'NONE', #30706, .T. ) ;
#51870=CARTESIAN_POINT ( 'NONE',  ( 5.193195059372482212E-16, -7.895640089090903757, -6.564402953523731377 ) ) ;
#51879=EDGE_CURVE ( 'NONE', #94099, #46925, #65923, .T. ) ;
#51882=CARTESIAN_POINT ( 'NONE',  ( 3.400000000000000355, 0.000000000000000000, -0.4455245229258316120 ) ) ;
#51928=ADVANCED_FACE ( 'NONE', ( #67321 ), #57593, .F. ) ;
#51995=CARTESIAN_POINT ( 'NONE',  ( 6.500000000000000000, 1.602771114417276932, -0.1495523863686145094 ) ) ;
#52129=DIRECTION ( 'NONE',  ( 0.000000000000000000, 0.000000000000000000, 1.000000000000000000 ) ) ;
#52148=CARTESIAN_POINT ( 'NONE',  ( -0.2813450144774459760, 7.667988119308860817, -6.122077150241857169 ) ) ;
#52231=AXIS2_PLACEMENT_3D ( 'NONE', #16617, #10118, #52697 ) ;
#52337=CARTESIAN_POINT ( 'NONE',  ( 0.000000000000000000, 0.000000000000000000, -0.4455245229258316120 ) ) ;
#52345=FACE_OUTER_BOUND ( 'NONE', #11223, .T. ) ;
#52383=AXIS2_PLACEMENT_3D ( 'NONE', #38241, #4252, #94872 ) ;
#52540=FILL_AREA_STYLE ('',( #13134 ) ) ;
#52549=ADVANCED_FACE ( 'NONE', ( #51790 ), #59381, .F. ) ;
#52554=CARTESIAN_POINT ( 'NONE',  ( 4.000000000000000000, 4.898587196589412829E-16, -2.296599999999999753 ) ) ;
#52561=ADVANCED_FACE ( 'NONE', ( #83623 ), #4109, .F. ) ;
#52653=ORIENTED_EDGE ( 'NONE', *, *, #6332, .T. ) ;
#52662=FACE_OUTER_BOUND ( 'NONE', #94093, .T. ) ;
#52697=DIRECTION ( 'NONE',  ( 1.000000000000000000, 0.000000000000000000, 0.000000000000000000 ) ) ;
#52701=EDGE_CURVE ( 'NONE', #15859, #38000, #1200, .T. ) ;
#52755=PRODUCT_DEFINITION_SHAPE ( 'NONE', 'NONE',  #39722 ) ;
#52791=AXIS2_PLACEMENT_3D ( 'NONE', #40853, #33321, #58095 ) ;
#52873=ADVANCED_FACE ( 'NONE', ( #28920 ), #91859, .F. ) ;
#52977=EDGE_CURVE ( 'NONE', #94655, #59491, #48807, .T. ) ;
#52992=DIRECTION ( 'NONE',  ( 0.000000000000000000, 0.000000000000000000, 1.000000000000000000 ) ) ;
#53011=EDGE_LOOP ( 'NONE', ( #37709, #49387, #32204, #18642, #13789, #52653, #18669 ) ) ;
#53051=DIRECTION ( 'NONE',  ( 0.000000000000000000, 0.000000000000000000, 1.000000000000000000 ) ) ;
#53125=CARTESIAN_POINT ( 'NONE',  ( -6.878751942472531411, 3.924677726130911815, -6.573129608219088205 ) ) ;
#53169=CARTESIAN_POINT ( 'NONE',  ( 0.000000000000000000, 0.000000000000000000, -2.296599999999999753 ) ) ;
#53214=ORIENTED_EDGE ( 'NONE', *, *, #86807, .T. ) ;
#53223=PRESENTATION_STYLE_ASSIGNMENT (( #3068 ) ) ;
#53261=DIRECTION ( 'NONE',  ( -0.8191520442889974607, 0.000000000000000000, -0.5735764363510379438 ) ) ;
#53266=AXIS2_PLACEMENT_3D ( 'NONE', #78542, #70986, #53740 ) ;
#53269=ORIENTED_EDGE ( 'NONE', *, *, #44034, .F. ) ;
#53271=AXIS2_PLACEMENT_3D ( 'NONE', #6258, #14883, #47776 ) ;
#53300=ORIENTED_EDGE ( 'NONE', *, *, #5283, .T. ) ;
#53484=EDGE_LOOP ( 'NONE', ( #68237, #48672, #26947, #23253 ) ) ;
#53511=ORIENTED_EDGE ( 'NONE', *, *, #93262, .F. ) ;
#53562=EDGE_CURVE ( 'NONE', #19817, #41440, #71293, .T. ) ;
#53573=CIRCLE ( 'NONE', #86314, 3.400000000000000355 ) ;
#53655=DIRECTION ( 'NONE',  ( -0.000000000000000000, -0.000000000000000000, -1.000000000000000000 ) ) ;
#53724=CARTESIAN_POINT ( 'NONE',  ( -6.499999999999999112, 3.752776749732556816, -8.000000000000000000 ) ) ;
#53740=DIRECTION ( 'NONE',  ( 1.000000000000000000, 0.000000000000000000, 0.000000000000000000 ) ) ;
#53859=EDGE_LOOP ( 'NONE', ( #195, #105964, #13854, #65137 ) ) ;
#53862=LINE ( 'NONE', #28044, #48498 ) ;
#53867=EDGE_LOOP ( 'NONE', ( #101370, #75062, #30530, #71275 ) ) ;
#54024=CARTESIAN_POINT ( 'NONE',  ( 6.499999999999999112, 3.752776749732595452, -0.7999999999999977129 ) ) ;
#54036=LINE ( 'NONE', #30338, #25279 ) ;
#54148=CARTESIAN_POINT ( 'NONE',  ( 0.2259792476677682238, -7.636022678937430364, -6.470294263593375561 ) ) ;
#54254=CARTESIAN_POINT ( 'NONE',  ( 5.727634848076682772, 4.575561887447793019, -6.326622577870439912 ) ) ;
#54284=ORIENTED_EDGE ( 'NONE', *, *, #56506, .F. ) ;
#54324=DIRECTION ( 'NONE',  ( -0.000000000000000000, -0.000000000000000000, -1.000000000000000000 ) ) ;
#54332=CARTESIAN_POINT ( 'NONE',  ( 0.000000000000000000, 0.000000000000000000, -6.418875477074183600 ) ) ;
#54386=AXIS2_PLACEMENT_3D ( 'NONE', #85011, #11095, #3023 ) ;
#54467=DIRECTION ( 'NONE',  ( 0.000000000000000000, 0.000000000000000000, 1.000000000000000000 ) ) ;
#54611=ORIENTED_EDGE ( 'NONE', *, *, #93699, .T. ) ;
#54633=VERTEX_POINT ( 'NONE', #85622 ) ;
#54650=SURFACE_STYLE_USAGE ( .BOTH. , #78945 ) ;
#54682=CARTESIAN_POINT ( 'NONE',  ( -0.8808064505793062882, -6.997019658119252306, -5.875704392893994488 ) ) ;
#54791=DIRECTION ( 'NONE',  ( 1.000000000000000000, 0.000000000000000000, 0.000000000000000000 ) ) ;
#54869=FACE_OUTER_BOUND ( 'NONE', #74788, .T. ) ;
#54879=ADVANCED_FACE ( 'NONE', ( #46091 ), #37945, .F. ) ;
#54891=ORIENTED_EDGE ( 'NONE', *, *, #17907, .T. ) ;
#54911=CARTESIAN_POINT ( 'NONE',  ( 0.000000000000000000, 0.000000000000000000, -6.838999999999999524 ) ) ;
#55033=EDGE_LOOP ( 'NONE', ( #69472, #35454, #80145, #60372 ) ) ;
#55079=LINE ( 'NONE', #64269, #99565 ) ;
#55114=ORIENTED_EDGE ( 'NONE', *, *, #31611, .F. ) ;
#55136=EDGE_LOOP ( 'NONE', ( #1446, #18069, #11319, #101629 ) ) ;
#55148=CARTESIAN_POINT ( 'NONE',  ( -3.250000000000016431, 5.629165124598842773, 1.734723475976807094E-15 ) ) ;
#55158=ORIENTED_EDGE ( 'NONE', *, *, #97255, .F. ) ;
#55202=FACE_OUTER_BOUND ( 'NONE', #102421, .T. ) ;
#55286=CARTESIAN_POINT ( 'NONE',  ( 6.500000000000007105, -3.752776749732581685, -0.7999999999999977129 ) ) ;
#55492=CARTESIAN_POINT ( 'NONE',  ( -2.352990130084491319E-16, 7.505553499465148271, -6.064240316920404439 ) ) ;
#55612=ORIENTED_EDGE ( 'NONE', *, *, #4591, .F. ) ;
#55622=DIRECTION ( 'NONE',  ( 0.000000000000000000, 0.000000000000000000, 1.000000000000000000 ) ) ;
#55635=ORIENTED_EDGE ( 'NONE', *, *, #2196, .T. ) ;
#55684=CARTESIAN_POINT ( 'NONE',  ( -6.499999999999996447, 1.286902272306384987, -0.09436334093185638761 ) ) ;
#55709=CARTESIAN_POINT ( 'NONE',  ( -6.499999999999999112, -3.752776749732587902, -6.064240316920403551 ) ) ;
#55734=CARTESIAN_POINT ( 'NONE',  ( -4.444974277458374701, -4.939246403833604582, -5.720331885005381700 ) ) ;
#55867=FACE_OUTER_BOUND ( 'NONE', #36348, .T. ) ;
#55912=CARTESIAN_POINT ( 'NONE',  ( 6.499999999999999112, 3.752776749732595452, -0.7999999999999977129 ) ) ;
#55931=EDGE_CURVE ( 'NONE', #57008, #26114, #64528, .T. ) ;
#55958=LINE ( 'NONE', #5325, #69938 ) ;
#56056=CARTESIAN_POINT ( 'NONE',  ( 0.000000000000000000, 0.000000000000000000, -1.581124522925831499 ) ) ;
#56057=DIRECTION ( 'NONE',  ( 1.000000000000000000, 0.000000000000000000, 0.000000000000000000 ) ) ;
#56080=DIRECTION ( 'NONE',  ( -0.000000000000000000, -0.000000000000000000, -1.000000000000000000 ) ) ;
#56105=ORIENTED_EDGE ( 'NONE', *, *, #93899, .F. ) ;
#56252=CARTESIAN_POINT ( 'NONE',  ( 0.000000000000000000, 0.000000000000000000, -1.161000000000000032 ) ) ;
#56277=ORIENTED_EDGE ( 'NONE', *, *, #14296, .T. ) ;
#56298=DIRECTION ( 'NONE',  ( 1.000000000000000000, 0.000000000000000000, 0.000000000000000000 ) ) ;
#56299=ORIENTED_EDGE ( 'NONE', *, *, #73735, .T. ) ;
#56305=CARTESIAN_POINT ( 'NONE',  ( 0.000000000000000000, 0.000000000000000000, -0.4455245229258316120 ) ) ;
#56365=EDGE_CURVE ( 'NONE', #13321, #34748, #43963, .T. ) ;
#56423=ORIENTED_EDGE ( 'NONE', *, *, #102202, .T. ) ;
#56425=DIRECTION ( 'NONE',  ( 0.000000000000000000, 0.000000000000000000, -1.000000000000000000 ) ) ;
#56427=DIRECTION ( 'NONE',  ( -0.000000000000000000, -0.000000000000000000, -1.000000000000000000 ) ) ;
#56478=ORIENTED_EDGE ( 'NONE', *, *, #67267, .F. ) ;
#56493=AXIS2_PLACEMENT_3D ( 'NONE', #68336, #13262, #40199 ) ;
#56506=EDGE_CURVE ( 'NONE', #27489, #96068, #12912, .T. ) ;
#56514=VERTEX_POINT ( 'NONE', #43588 ) ;
#56519=CIRCLE ( 'NONE', #104820, 3.400000000000000355 ) ;
#56599=CARTESIAN_POINT ( 'NONE',  ( -6.831985876597696183, 3.295913427296334408, -6.443925148804114045 ) ) ;
#56605=FACE_OUTER_BOUND ( 'NONE', #37224, .T. ) ;
#56609=ORIENTED_EDGE ( 'NONE', *, *, #35977, .T. ) ;
#56661=AXIS2_PLACEMENT_3D ( 'NONE', #68279, #100632, #67224 ) ;
#56730=CIRCLE ( 'NONE', #70536, 0.6186547224754559426 ) ;
#56866=LINE ( 'NONE', #1271, #41381 ) ;
#56999=B_SPLINE_CURVE_WITH_KNOTS ( 'NONE', 3,
 ( #6069, #22299, #95110, #88598, #97204, #29339 ),
 .UNSPECIFIED., .F., .F.,
 ( 4, 2, 4 ),
 ( 0.000000000000000000, 0.0003352299596267559732, 0.0006704599192535119464 ),
 .UNSPECIFIED. ) ;
#57008=VERTEX_POINT ( 'NONE', #6835 ) ;
#57033=DIRECTION ( 'NONE',  ( 0.000000000000000000, 0.000000000000000000, 1.000000000000000000 ) ) ;
#57039=ADVANCED_FACE ( 'NONE', ( #15459 ), #1030, .T. ) ;
#57062=ADVANCED_FACE ( 'NONE', ( #85945 ), #42800, .T. ) ;
#57063=FACE_OUTER_BOUND ( 'NONE', #64474, .T. ) ;
#57219=ORIENTED_EDGE ( 'NONE', *, *, #91953, .F. ) ;
#57571=ORIENTED_EDGE ( 'NONE', *, *, #98343, .F. ) ;
#57572=AXIS2_PLACEMENT_3D ( 'NONE', #71555, #97417, #80179 ) ;
#57593=CYLINDRICAL_SURFACE ( 'NONE', #71078, 3.400000000000000355 ) ;
#57613=ORIENTED_EDGE ( 'NONE', *, *, #60962, .T. ) ;
#57624=CARTESIAN_POINT ( 'NONE',  ( 6.500000000000002665, 2.501851166488368694, -5.848636054922034866 ) ) ;
#57676=CIRCLE ( 'NONE', #2561, 3.400000000000000355 ) ;
#57696=EDGE_LOOP ( 'NONE', ( #84178, #56478 ) ) ;
#57703=ADVANCED_FACE ( 'NONE', ( #33356 ), #106144, .F. ) ;
#57718=VECTOR ( 'NONE', #88438, 1000.000000000000000 ) ;
#57725=DIRECTION ( 'NONE',  ( -0.8191520442889881348, 1.003171929053520186E-16, 0.5735764363510513775 ) ) ;
#57843=ADVANCED_FACE ( 'NONE', ( #13953 ), #37303, .T. ) ;
#57847=LINE ( 'NONE', #98327, #104276 ) ;
#57855=EDGE_CURVE ( 'NONE', #102954, #37530, #21820, .T. ) ;
#57973=ORIENTED_EDGE ( 'NONE', *, *, #72818, .F. ) ;
#57992=VECTOR ( 'NONE', #43734, 1000.000000000000000 ) ;
#58095=DIRECTION ( 'NONE',  ( -1.000000000000000000, 0.000000000000000000, 0.000000000000000000 ) ) ;
#58106=DIRECTION ( 'NONE',  ( -0.000000000000000000, -0.000000000000000000, -1.000000000000000000 ) ) ;
#58140=ORIENTED_EDGE ( 'NONE', *, *, #74725, .F. ) ;
#58168=DIRECTION ( 'NONE',  ( -1.000000000000000000, 0.000000000000000000, 0.000000000000000000 ) ) ;
#58244=CARTESIAN_POINT ( 'NONE',  ( -3.400000000000000355, 4.163799117101001052E-16, -4.987924522925830217 ) ) ;
#58269=ORIENTED_EDGE ( 'NONE', *, *, #101671, .F. ) ;
#58365=CARTESIAN_POINT ( 'NONE',  ( -6.815830331203684977, -1.215378054691643734E-13, -6.171384342982610072 ) ) ;
#58374=CIRCLE ( 'NONE', #11861, 4.000000000000000000 ) ;
#58419=VECTOR ( 'NONE', #16455, 1000.000000000000000 ) ;
#58512=FACE_OUTER_BOUND ( 'NONE', #268, .T. ) ;
#58601=ORIENTED_EDGE ( 'NONE', *, *, #5265, .T. ) ;
#58710=ORIENTED_EDGE ( 'NONE', *, *, #84004, .T. ) ;
#58824=CARTESIAN_POINT ( 'NONE',  ( 4.000000000000000000, 4.898587196589412829E-16, -4.567799999999999194 ) ) ;
#58845=DIRECTION ( 'NONE',  ( -1.000000000000000000, 0.000000000000000000, 0.000000000000000000 ) ) ;
#58850=CARTESIAN_POINT ( 'NONE',  ( 4.000000000000000000, 4.898587196589412829E-16, -2.296599999999999753 ) ) ;
#58856=CARTESIAN_POINT ( 'NONE',  ( -6.815830331203684977, -1.215378054691643734E-13, -6.171384342982610072 ) ) ;
#58954=FACE_OUTER_BOUND ( 'NONE', #11323, .T. ) ;
#58961=CONICAL_SURFACE ( 'NONE', #96852, 3.400000000000000355, 0.9599310885968748153 ) ;
#59031=ORIENTED_EDGE ( 'NONE', *, *, #80906, .F. ) ;
#59072=DIRECTION ( 'NONE',  ( 0.000000000000000000, -1.000000000000000000, 0.000000000000000000 ) ) ;
#59201=CARTESIAN_POINT ( 'NONE',  ( -3.400000000000000355, 4.163799117101001052E-16, -0.4455245229258316120 ) ) ;
#59208=CARTESIAN_POINT ( 'NONE',  ( -2.141486166123598434, 6.269165884987821791, -0.07763482564820649301 ) ) ;
#59231=DIRECTION ( 'NONE',  ( 0.000000000000000000, 0.000000000000000000, 1.000000000000000000 ) ) ;
#59283=FACE_OUTER_BOUND ( 'NONE', #51247, .T. ) ;
#59381=CYLINDRICAL_SURFACE ( 'NONE', #100473, 4.000000000000001776 ) ;
#59459=ORIENTED_EDGE ( 'NONE', *, *, #72817, .F. ) ;
#59491=VERTEX_POINT ( 'NONE', #71419 ) ;
#59583=CARTESIAN_POINT ( 'NONE',  ( 6.500000000000000000, 2.536640449112291140, -0.3753468889000200481 ) ) ;
#59668=EDGE_LOOP ( 'NONE', ( #15453, #23613, #14916 ) ) ;
#59724=DIRECTION ( 'NONE',  ( 1.000000000000000000, 0.000000000000000000, 0.000000000000000000 ) ) ;
#59739=CARTESIAN_POINT ( 'NONE',  ( -5.698650001973517121, 4.592339236403556235, -6.344532336093704039 ) ) ;
#60008=CARTESIAN_POINT ( 'NONE',  ( 6.837824896291513355, -3.947820044545448326, -6.564402953523719830 ) ) ;
#60021=CARTESIAN_POINT ( 'NONE',  ( 3.400000000000000355, 0.000000000000000000, -7.554475477074167777 ) ) ;
#60027=CARTESIAN_POINT ( 'NONE',  ( 1.058054217398698871, -6.894685612232814620, -0.3576316571898649488 ) ) ;
#60114=DIRECTION ( 'NONE',  ( -1.000000000000000000, 0.000000000000000000, 0.000000000000000000 ) ) ;
#60133=CARTESIAN_POINT ( 'NONE',  ( -6.815962252199544658, 1.383413844632507717, -6.173425845474766582 ) ) ;
#60188=DIRECTION ( 'NONE',  ( -0.000000000000000000, -0.000000000000000000, -1.000000000000000000 ) ) ;
#60281=CARTESIAN_POINT ( 'NONE',  ( 0.000000000000000000, 0.000000000000000000, -8.000000000000000000 ) ) ;
#60372=ORIENTED_EDGE ( 'NONE', *, *, #65905, .F. ) ;
#60511=DIRECTION ( 'NONE',  ( 1.000000000000000000, 0.000000000000000000, 0.000000000000000000 ) ) ;
#60579=FACE_OUTER_BOUND ( 'NONE', #88751, .T. ) ;
#60605=LINE ( 'NONE', #103172, #71685 ) ;
#60619=ORIENTED_EDGE ( 'NONE', *, *, #55931, .T. ) ;
#60637=DIRECTION ( 'NONE',  ( -1.000000000000000000, 0.000000000000000000, 0.000000000000000000 ) ) ;
#60686=DIRECTION ( 'NONE',  ( 0.000000000000000000, 0.000000000000000000, 1.000000000000000000 ) ) ;
#60744=VECTOR ( 'NONE', #722, 1000.000000000000000 ) ;
#60759=ORIENTED_EDGE ( 'NONE', *, *, #101671, .T. ) ;
#60798=DIRECTION ( 'NONE',  ( -0.000000000000000000, -0.000000000000000000, -1.000000000000000000 ) ) ;
#60799=CARTESIAN_POINT ( 'NONE',  ( -0.04050535873993734576, 7.919512791578242172, -6.573129608219096198 ) ) ;
#60809=TOROIDAL_SURFACE ( 'NONE', #52231, 8.331345277524542681, 0.6186547224754556096 ) ;
#60814=DIRECTION ( 'NONE',  ( -0.8191520442889924647, 0.000000000000000000, -0.5735764363510451602 ) ) ;
#60847=AXIS2_PLACEMENT_3D ( 'NONE', #56252, #39588, #21297 ) ;
#60962=EDGE_CURVE ( 'NONE', #18921, #72570, #3142, .T. ) ;
#60971=CARTESIAN_POINT ( 'NONE',  ( 0.000000000000000000, 0.000000000000000000, -6.123524522925831270 ) ) ;
#61053=CARTESIAN_POINT ( 'NONE',  ( 6.815830331203684977, 1.210606185736183200E-13, -6.171384342982610072 ) ) ;
#61084=ORIENTED_EDGE ( 'NONE', *, *, #70339, .T. ) ;
#61188=CARTESIAN_POINT ( 'NONE',  ( 6.815964470353729432, -1.383691465877838755, -6.173460172893358688 ) ) ;
#61234=EDGE_CURVE ( 'NONE', #104748, #17654, #89221, .T. ) ;
#61249=CARTESIAN_POINT ( 'NONE',  ( 0.000000000000000000, 0.000000000000000000, -7.259124522925831435 ) ) ;
#61336=ORIENTED_EDGE ( 'NONE', *, *, #25782, .F. ) ;
#61405=DIRECTION ( 'NONE',  ( 0.000000000000000000, 0.000000000000000000, 1.000000000000000000 ) ) ;
#61459=ORIENTED_EDGE ( 'NONE', *, *, #81840, .T. ) ;
#61544=CARTESIAN_POINT ( 'NONE',  ( 0.000000000000000000, 0.000000000000000000, -7.381345277524544279 ) ) ;
#61547=( BOUNDED_SURFACE ( )  B_SPLINE_SURFACE ( 3, 2, ( 
 ( #25711, #25158, #32717 ),
 ( #8404, #6814, #106026 ),
 ( #98473, #65055, #80692 ),
 ( #273, #65586, #66652 ),
 ( #106567, #15972, #33241 ),
 ( #24626, #7335, #98994 ) ),
 .UNSPECIFIED., .F., .F., .F. ) 
 B_SPLINE_SURFACE_WITH_KNOTS ( ( 4, 2, 4 ),
 ( 3, 3 ),
 ( 0.003190620565844237266, 0.007281897438794509257, 0.01137317431174478082 ),
 ( 0.000000000000000000, 1.000000000000000000 ),
 .UNSPECIFIED. ) 
 GEOMETRIC_REPRESENTATION_ITEM ( )  RATIONAL_B_SPLINE_SURFACE ( (
 ( 1.000000000000000000, 0.8047731410850398337, 1.000000000000000000),
 ( 1.000000000000000000, 0.8125552299156226788, 1.000000000000000000),
 ( 1.000000000000000000, 0.8191520442889870246, 1.000000000000000000),
 ( 1.000000000000000000, 0.8191520442889870246, 1.000000000000000000),
 ( 1.000000000000000000, 0.8125552299156239000, 1.000000000000000000),
 ( 1.000000000000000000, 0.8047731410850399447, 1.000000000000000000) ) ) 
 REPRESENTATION_ITEM ( '' )  SURFACE ( )  );
#61587=DIRECTION ( 'NONE',  ( 0.000000000000000000, 0.000000000000000000, 1.000000000000000000 ) ) ;
#61649=ADVANCED_FACE ( 'NONE', ( #52345 ), #2366, .F. ) ;
#61676=DIRECTION ( 'NONE',  ( 0.000000000000000000, 0.000000000000000000, 1.000000000000000000 ) ) ;
#61769=CARTESIAN_POINT ( 'NONE',  ( -2.075968632160785088, 6.306992450857870303, -6.056431503346635381 ) ) ;
#61835=ORIENTED_EDGE ( 'NONE', *, *, #93699, .F. ) ;
#61872=CARTESIAN_POINT ( 'NONE',  ( 4.444974277458376477, 4.939246403833576160, -5.720331885005371930 ) ) ;
#62056=ORIENTED_EDGE ( 'NONE', *, *, #95539, .F. ) ;
#62074=ORIENTED_EDGE ( 'NONE', *, *, #36837, .T. ) ;
#62092=DIRECTION ( 'NONE',  ( 1.000000000000000000, 0.000000000000000000, 0.000000000000000000 ) ) ;
#62130=CARTESIAN_POINT ( 'NONE',  ( 3.400000000000000355, 0.000000000000000000, -8.000000000000000000 ) ) ;
#62131=CARTESIAN_POINT ( 'NONE',  ( 5.698650001973516233, -4.592339236403583769, -6.344532336093709368 ) ) ;
#62135=CARTESIAN_POINT ( 'NONE',  ( 2.688402820137708371, 5.953403407568484518, -0.01956314070068211619 ) ) ;
#62170=DIRECTION ( 'NONE',  ( 1.000000000000000000, 0.000000000000000000, 0.000000000000000000 ) ) ;
#62187=CARTESIAN_POINT ( 'NONE',  ( -4.555094537983155334, -5.243183837310271045, -6.208110906918266281 ) ) ;
#62276=ADVANCED_FACE ( 'NONE', ( #5932 ), #88681, .F. ) ;
#62288=CARTESIAN_POINT ( 'NONE',  ( -6.781345014477443200, -3.590342129888875355, -6.122077150241855392 ) ) ;
#62293=CARTESIAN_POINT ( 'NONE',  ( -4.000000000000000888, 4.898587196589413815E-16, 3.469446951953614189E-15 ) ) ;
#62306=LINE ( 'NONE', #81107, #13808 ) ;
#62309=ADVANCED_FACE ( 'NONE', ( #88994 ), #31881, .F. ) ;
#62443=ORIENTED_EDGE ( 'NONE', *, *, #76970, .F. ) ;
#62495=ORIENTED_EDGE ( 'NONE', *, *, #77774, .F. ) ;
#62567=ORIENTED_EDGE ( 'NONE', *, *, #38555, .F. ) ;
#62592=DIRECTION ( 'NONE',  ( 0.8191520442889881348, 0.000000000000000000, 0.5735764363510513775 ) ) ;
#62621=AXIS2_PLACEMENT_3D ( 'NONE', #2166, #10271, #58845 ) ;
#62654=AXIS2_PLACEMENT_3D ( 'NONE', #77876, #69785, #3454 ) ;
#62776=LINE ( 'NONE', #5581, #72056 ) ;
#62810=CARTESIAN_POINT ( 'NONE',  ( -2.055025722541617750, -6.319083845364160013, -5.720331885005381700 ) ) ;
#62814=CARTESIAN_POINT ( 'NONE',  ( -0.8808064505792063681, 6.997019658119279839, -5.875704392892937555 ) ) ;
#62903=VERTEX_POINT ( 'NONE', #63281 ) ;
#62907=DIRECTION ( 'NONE',  ( -1.000000000000000000, 0.000000000000000000, 0.000000000000000000 ) ) ;
#62920=CARTESIAN_POINT ( 'NONE',  ( 1.098735407080511761, 7.248058225761106144, -6.326622577871084729 ) ) ;
#62991=DIRECTION ( 'NONE',  ( 1.000000000000000000, 0.000000000000000000, 0.000000000000000000 ) ) ;
#63099=CARTESIAN_POINT ( 'NONE',  ( 1.127757440534756794, 7.231345287187100013, -6.344532336093711145 ) ) ;
#63125=DIRECTION ( 'NONE',  ( -0.000000000000000000, -0.000000000000000000, 1.000000000000000000 ) ) ;
#63223=ORIENTED_EDGE ( 'NONE', *, *, #70808, .T. ) ;
#63281=CARTESIAN_POINT ( 'NONE',  ( -4.000000000000000000, 0.000000000000000000, -3.432199999999999918 ) ) ;
#63387=CARTESIAN_POINT ( 'NONE',  ( 0.000000000000000000, 0.000000000000000000, -0.4455245229258316120 ) ) ;
#63450=LINE ( 'NONE', #15931, #58419 ) ;
#63542=ORIENTED_EDGE ( 'NONE', *, *, #61234, .F. ) ;
#63611=CARTESIAN_POINT ( 'NONE',  ( 0.000000000000000000, 0.000000000000000000, -0.02540000000000007530 ) ) ;
#63660=CARTESIAN_POINT ( 'NONE',  ( 6.826399921716641117, 2.638123634694619746, -6.344399053232583796 ) ) ;
#63724=CARTESIAN_POINT ( 'NONE',  ( 6.499999999999999112, 1.355443906731582659, -5.756734754743127347 ) ) ;
#63761=CARTESIAN_POINT ( 'NONE',  ( -5.699988423468465903, -4.591578518468272030, -6.344710093416088270 ) ) ;
#63785=CONICAL_SURFACE ( 'NONE', #27875, 3.340000000000000746, 0.9599310885968781459 ) ;
#63808=DIRECTION ( 'NONE',  ( -1.000000000000000000, 0.000000000000000000, 0.000000000000000000 ) ) ;
#63833=ORIENTED_EDGE ( 'NONE', *, *, #41416, .T. ) ;
#63975=LINE ( 'NONE', #7293, #68764 ) ;
#64173=CARTESIAN_POINT ( 'NONE',  ( 2.832728918602883450, 6.234773369952728572, -6.171481112545254000 ) ) ;
#64237=DIRECTION ( 'NONE',  ( 0.000000000000000000, 0.000000000000000000, 1.000000000000000000 ) ) ;
#64269=CARTESIAN_POINT ( 'NONE',  ( -4.000000000000001776, 4.898587196589415787E-16, -25.03750572909317285 ) ) ;
#64322=B_SPLINE_CURVE_WITH_KNOTS ( 'NONE', 3,
 ( #22240, #70238, #20140, #3379, #95576, #54024 ),
 .UNSPECIFIED., .F., .F.,
 ( 4, 2, 4 ),
 ( 0.003841072314098378879, 0.005765657563962189869, 0.007690242813826001292 ),
 .UNSPECIFIED. ) ;
#64407=CARTESIAN_POINT ( 'NONE',  ( -2.868955696345051593E-16, 7.505553499465148271, -6.177802698399965209 ) ) ;
#64461=ADVANCED_FACE ( 'NONE', ( #6247 ), #85538, .F. ) ;
#64474=EDGE_LOOP ( 'NONE', ( #73398, #71065, #55158, #6404 ) ) ;
#64489=CARTESIAN_POINT ( 'NONE',  ( -6.663120783604504993, -3.846954578057071750, -6.460786012260017586 ) ) ;
#64493=AXIS2_PLACEMENT_3D ( 'NONE', #93288, #2663, #76024 ) ;
#64514=CARTESIAN_POINT ( 'NONE',  ( 0.000000000000000000, 0.000000000000000000, -4.987924522925830217 ) ) ;
#64528=CIRCLE ( 'NONE', #42183, 3.400000000000000355 ) ;
#64557=VERTEX_POINT ( 'NONE', #98968 ) ;
#64559=AXIS2_PLACEMENT_3D ( 'NONE', #50158, #83064, #17810 ) ;
#64612=DIRECTION ( 'NONE',  ( 0.000000000000000000, 0.000000000000000000, 1.000000000000000000 ) ) ;
#64661=AXIS2_PLACEMENT_3D ( 'NONE', #60971, #85787, #93857 ) ;
#64677=CARTESIAN_POINT ( 'NONE',  ( 3.400000000000000355, 0.000000000000000000, -0.4455245229258316120 ) ) ;
#64818=AXIS2_PLACEMENT_3D ( 'NONE', #90506, #73779, #106680 ) ;
#64870=ORIENTED_EDGE ( 'NONE', *, *, #36887, .T. ) ;
#64960=CARTESIAN_POINT ( 'NONE',  ( 3.400000000000000355, 0.000000000000000000, -6.123524522925831270 ) ) ;
#65012=FACE_OUTER_BOUND ( 'NONE', #55136, .T. ) ;
#65055=CARTESIAN_POINT ( 'NONE',  ( 2.075968632161603100, -6.306992450857173971, -6.056431503346049183 ) ) ;
#65071=DIRECTION ( 'NONE',  ( -1.000000000000000000, 0.000000000000000000, 0.000000000000000000 ) ) ;
#65072=AXIS2_PLACEMENT_3D ( 'NONE', #79156, #54324, #95351 ) ;
#65078=DIRECTION ( 'NONE',  ( 0.000000000000000000, 0.000000000000000000, -1.000000000000000000 ) ) ;
#65137=ORIENTED_EDGE ( 'NONE', *, *, #51879, .F. ) ;
#65144=CARTESIAN_POINT ( 'NONE',  ( -1.083333333333333703, 6.880090707843048214, -5.848636054922038419 ) ) ;
#65178=DIRECTION ( 'NONE',  ( -0.000000000000000000, -0.000000000000000000, -1.000000000000000000 ) ) ;
#65186=CARTESIAN_POINT ( 'NONE',  ( 0.000000000000000000, 0.000000000000000000, -3.432199999999999918 ) ) ;
#65231=CARTESIAN_POINT ( 'NONE',  ( 5.007715329123895321E-16, -7.505553499465175804, -6.064240316920414209 ) ) ;
#65557=VECTOR ( 'NONE', #21597, 1000.000000000000000 ) ;
#65576=UNCERTAINTY_MEASURE_WITH_UNIT (LENGTH_MEASURE( 1.000000000000000082E-05 ), #85460, 'distance_accuracy_value', 'NONE');
#65586=CARTESIAN_POINT ( 'NONE',  ( 4.424031367838395568, -4.951337798340586183, -6.056431503346049183 ) ) ;
#65633=ORIENTED_EDGE ( 'NONE', *, *, #29911, .F. ) ;
#65728=CARTESIAN_POINT ( 'NONE',  ( -6.499999999999999112, 3.752776749732556816, -0.7999999999999821698 ) ) ;
#65821=CARTESIAN_POINT ( 'NONE',  ( 6.826581433397953980, -2.695947255479825166, -6.331032031596339316 ) ) ;
#65850=FACE_OUTER_BOUND ( 'NONE', #106749, .T. ) ;
#65905=EDGE_CURVE ( 'NONE', #59491, #48619, #41389, .T. ) ;
#65920=AXIS2_PLACEMENT_3D ( 'NONE', #25260, #24724, #2004 ) ;
#65923=CIRCLE ( 'NONE', #19464, 4.000000000000000000 ) ;
#65954=EDGE_CURVE ( 'NONE', #83820, #9879, #90667, .T. ) ;
#65986=ORIENTED_EDGE ( 'NONE', *, *, #36887, .F. ) ;
#66169=ADVANCED_FACE ( 'NONE', ( #52662 ), #102284, .T. ) ;
#66211=CARTESIAN_POINT ( 'NONE',  ( -6.499999999999999112, -3.752776749732587902, -8.000000000000000000 ) ) ;
#66334=DIRECTION ( 'NONE',  ( -1.000000000000000000, 0.000000000000000000, 0.000000000000000000 ) ) ;
#66357=CONICAL_SURFACE ( 'NONE', #102559, 4.000000000000000000, 0.9599310885968912466 ) ;
#66395=CARTESIAN_POINT ( 'NONE',  ( -3.400000000000000355, 4.163799117101001052E-16, -3.852324522925831385 ) ) ;
#66495=EDGE_CURVE ( 'NONE', #5468, #39998, #71786, .T. ) ;
#66512=AXIS2_PLACEMENT_3D ( 'NONE', #92403, #18551, #75693 ) ;
#66603=VECTOR ( 'NONE', #90957, 1000.000000000000000 ) ;
#66652=CARTESIAN_POINT ( 'NONE',  ( 4.574783636564311529, -5.228990388888064444, -6.171384342982683791 ) ) ;
#66791=CIRCLE ( 'NONE', #18623, 3.400000000000000355 ) ;
#66803=ORIENTED_EDGE ( 'NONE', *, *, #5543, .T. ) ;
#66942=CARTESIAN_POINT ( 'NONE',  ( -6.815830331203685866, -0.6619522098568515478, -6.171384342982615401 ) ) ;
#67034=CARTESIAN_POINT ( 'NONE',  ( -4.466912950640278268E-14, -7.505553499465147382, -0.7999999999999977129 ) ) ;
#67067=AXIS2_PLACEMENT_3D ( 'NONE', #17062, #99551, #25727 ) ;
#67096=ORIENTED_EDGE ( 'NONE', *, *, #26052, .T. ) ;
#67101=ORIENTED_EDGE ( 'NONE', *, *, #18382, .T. ) ;
#67132=CARTESIAN_POINT ( 'NONE',  ( -6.499999999999999112, -1.336926445781680739, -6.054363369342814494 ) ) ;
#67201=B_SPLINE_CURVE_WITH_KNOTS ( 'NONE', 3,
 ( #27245, #25649, #91417, #1296, #51995, #50392, #59583, #42850, #83304, #34797 ),
 .UNSPECIFIED., .F., .F.,
 ( 4, 2, 2, 2, 4 ),
 ( 0.009353627468483458399, 0.01031000219096075976, 0.01126637691343805939, 0.01222275163591535901, 0.01317912635839266038 ),
 .UNSPECIFIED. ) ;
#67221=ORIENTED_EDGE ( 'NONE', *, *, #13288, .T. ) ;
#67224=DIRECTION ( 'NONE',  ( -1.000000000000000000, 1.224646799147351482E-16, 0.000000000000000000 ) ) ;
#67260=ORIENTED_EDGE ( 'NONE', *, *, #71996, .F. ) ;
#67267=EDGE_CURVE ( 'NONE', #71589, #40596, #15131, .T. ) ;
#67268=ORIENTED_EDGE ( 'NONE', *, *, #2418, .F. ) ;
#67283=VERTEX_POINT ( 'NONE', #18766 ) ;
#67321=FACE_OUTER_BOUND ( 'NONE', #70010, .T. ) ;
#67341=EDGE_LOOP ( 'NONE', ( #99689, #29859, #83665, #4292 ) ) ;
#67373=CYLINDRICAL_SURFACE ( 'NONE', #90617, 3.400000000000000355 ) ;
#67384=EDGE_CURVE ( 'NONE', #41440, #19817, #92594, .T. ) ;
#67474=CARTESIAN_POINT ( 'NONE',  ( 4.000000000000000000, 4.898587196589412829E-16, -3.432199999999999918 ) ) ;
#67486=ORIENTED_EDGE ( 'NONE', *, *, #48128, .T. ) ;
#67530=ORIENTED_EDGE ( 'NONE', *, *, #61234, .T. ) ;
#67667=DIRECTION ( 'NONE',  ( -1.000000000000000000, 0.000000000000000000, 0.000000000000000000 ) ) ;
#67682=CARTESIAN_POINT ( 'NONE',  ( 4.000000000000000888, 0.000000000000000000, 3.469446951953614189E-15 ) ) ;
#67738=DIRECTION ( 'NONE',  ( 0.000000000000000000, 0.000000000000000000, -1.000000000000000000 ) ) ;
#67837=ORIENTED_EDGE ( 'NONE', *, *, #74743, .F. ) ;
#67857=CARTESIAN_POINT ( 'NONE',  ( 4.000000000000001776, 0.000000000000000000, -25.03750572909317285 ) ) ;
#68029=ADVANCED_FACE ( 'NONE', ( #90633 ), #47648, .F. ) ;
#68128=ORIENTED_EDGE ( 'NONE', *, *, #21556, .T. ) ;
#68212=B_SPLINE_CURVE_WITH_KNOTS ( 'NONE', 3,
 ( #102314, #4160, #11694, #77517, #20398, #95826, #95297, #38150 ),
 .UNSPECIFIED., .F., .F.,
 ( 4, 2, 2, 4 ),
 ( 2.459764731290589165E-07, 0.001920659145285759243, 0.002880865729692073940, 0.003841072314098388854 ),
 .UNSPECIFIED. ) ;
#68237=ORIENTED_EDGE ( 'NONE', *, *, #32944, .F. ) ;
#68279=CARTESIAN_POINT ( 'NONE',  ( -8.331345277524542681, 1.020295532671184640E-15, -7.381345277524544279 ) ) ;
#68291=PRODUCT_DEFINITION_CONTEXT ( 'detailed design', #39724, 'design' ) ;
#68314=EDGE_CURVE ( 'NONE', #100791, #80953, #70347, .T. ) ;
#68336=CARTESIAN_POINT ( 'NONE',  ( 0.000000000000000000, 0.000000000000000000, 1.734723475976807094E-15 ) ) ;
#68409=CARTESIAN_POINT ( 'NONE',  ( 0.000000000000000000, 0.000000000000000000, -6.123524522925831270 ) ) ;
#68462=AXIS2_PLACEMENT_3D ( 'NONE', #96263, #105906, #22912 ) ;
#68488=CARTESIAN_POINT ( 'NONE',  ( -2.352990130084491319E-16, 7.505553499465148271, -8.000000000000000000 ) ) ;
#68505=AXIS2_PLACEMENT_3D ( 'NONE', #60281, #60798, #10620 ) ;
#68528=CIRCLE ( 'NONE', #56493, 6.500000000000000888 ) ;
#68562=CIRCLE ( 'NONE', #80538, 4.000000000000002665 ) ;
#68602=CARTESIAN_POINT ( 'NONE',  ( -3.400000000000000355, 4.163799117101001052E-16, -4.147675477074182382 ) ) ;
#68622=CARTESIAN_POINT ( 'NONE',  ( 6.831985876597696183, -3.295913427296359277, -6.443925148804115821 ) ) ;
#68702=DIRECTION ( 'NONE',  ( -1.000000000000000000, 0.000000000000000000, 0.000000000000000000 ) ) ;
#68761=ORIENTED_EDGE ( 'NONE', *, *, #56506, .T. ) ;
#68764=VECTOR ( 'NONE', #80125, 1000.000000000000114 ) ;
#68778=CARTESIAN_POINT ( 'NONE',  ( 0.000000000000000000, 0.000000000000000000, -3.852324522925831385 ) ) ;
#68802=B_SPLINE_CURVE_WITH_KNOTS ( 'NONE', 3,
 ( #101259, #42469, #59208, #76966, #50547, #9032 ),
 .UNSPECIFIED., .F., .F.,
 ( 4, 2, 4 ),
 ( 0.003841072314098338547, 0.005765657563962176858, 0.007690242813826015170 ),
 .UNSPECIFIED. ) ;
#68844=AXIS2_PLACEMENT_3D ( 'NONE', #101066, #10453, #60637 ) ;
#68896=CARTESIAN_POINT ( 'NONE',  ( 4.424031367839869944, 4.951337798340052387, -6.056431503346638046 ) ) ;
#69041=CARTESIAN_POINT ( 'NONE',  ( 3.528928113779659093, -5.468125903023639545, -1.782684363745784063E-14 ) ) ;
#69095=AXIS2_PLACEMENT_3D ( 'NONE', #96768, #5100, #6675 ) ;
#69144=CONICAL_SURFACE ( 'NONE', #27971, 4.000000000000000000, 0.9599310885968912466 ) ;
#69165=EDGE_CURVE ( 'NONE', #3656, #86116, #40500, .T. ) ;
#69197=CARTESIAN_POINT ( 'NONE',  ( 0.000000000000000000, 0.000000000000000000, -8.000000000000000000 ) ) ;
#69224=ORIENTED_EDGE ( 'NONE', *, *, #39683, .F. ) ;
#69274=CARTESIAN_POINT ( 'NONE',  ( -6.499999999999999112, -4.077972562205410156, -6.122137109124706988 ) ) ;
#69280=ORIENTED_EDGE ( 'NONE', *, *, #71142, .F. ) ;
#69310=CARTESIAN_POINT ( 'NONE',  ( -12.99999999999996625, -1.778091562876227272E-14, -8.000000000000000000 ) ) ;
#69326=CARTESIAN_POINT ( 'NONE',  ( 0.000000000000000000, 0.000000000000000000, -3.012075477074183105 ) ) ;
#69416=FILL_AREA_STYLE ('',( #12744 ) ) ;
#69435=CARTESIAN_POINT ( 'NONE',  ( -4.000000000000002665, 0.000000000000000000, -7.974599999999995248 ) ) ;
#69451=CARTESIAN_POINT ( 'NONE',  ( -4.000000000000000000, 0.000000000000000000, -0.02540000000000007530 ) ) ;
#69472=ORIENTED_EDGE ( 'NONE', *, *, #102673, .T. ) ;
#69496=DIRECTION ( 'NONE',  ( -0.000000000000000000, -0.000000000000000000, -1.000000000000000000 ) ) ;
#69776=VECTOR ( 'NONE', #104623, 1000.000000000000114 ) ;
#69785=DIRECTION ( 'NONE',  ( -0.000000000000000000, -0.000000000000000000, 1.000000000000000000 ) ) ;
#69831=CARTESIAN_POINT ( 'NONE',  ( -4.574783636564919931, -5.228990388887491569, -6.171384342982614513 ) ) ;
#69847=CARTESIAN_POINT ( 'NONE',  ( -3.400000000000000355, 4.163799117101001052E-16, -1.581124522925831499 ) ) ;
#69937=( NAMED_UNIT ( * ) SI_UNIT ( $, .STERADIAN. ) SOLID_ANGLE_UNIT ( ) );
#69938=VECTOR ( 'NONE', #71110, 1000.000000000000000 ) ;
#70010=EDGE_LOOP ( 'NONE', ( #9303, #58601, #25847, #1810 ) ) ;
#70197=CARTESIAN_POINT ( 'NONE',  ( 8.673617379884035472E-16, 7.505553499465148271, -0.7999999999999977129 ) ) ;
#70238=CARTESIAN_POINT ( 'NONE',  ( 3.809068165403731943, 5.306386968807657034, 1.196857554470325985E-15 ) ) ;
#70336=( LENGTH_UNIT ( ) NAMED_UNIT ( * ) SI_UNIT ( .MILLI., .METRE. ) );
#70339=EDGE_CURVE ( 'NONE', #717, #82973, #62306, .T. ) ;
#70340=VECTOR ( 'NONE', #88735, 1000.000000000000000 ) ;
#70347=CIRCLE ( 'NONE', #99665, 4.000000000000000000 ) ;
#70360=ORIENTED_EDGE ( 'NONE', *, *, #100708, .F. ) ;
#70365=CARTESIAN_POINT ( 'NONE',  ( -4.424031367839510231, -4.951337798339865870, -6.056431503346049183 ) ) ;
#70371=CARTESIAN_POINT ( 'NONE',  ( -4.574783636564536238, 5.228990388887307716, -6.171384342982487503 ) ) ;
#70536=AXIS2_PLACEMENT_3D ( 'NONE', #100575, #59072, #91957 ) ;
#70538=CARTESIAN_POINT ( 'NONE',  ( 3.981862520314373377, 0.000000000000000000, -0.01269999999999786924 ) ) ;
#70568=VERTEX_POINT ( 'NONE', #55492 ) ;
#70646=CARTESIAN_POINT ( 'NONE',  ( 6.499999999999996447, 3.752776749732559036, -6.177805531629057434 ) ) ;
#70678=EDGE_CURVE ( 'NONE', #14310, #46925, #31792, .T. ) ;
#70707=VECTOR ( 'NONE', #37966, 1000.000000000000000 ) ;
#70751=CARTESIAN_POINT ( 'NONE',  ( 3.249999999999998668, 5.629165124598852543, -5.592027715088707218 ) ) ;
#70765=CYLINDRICAL_SURFACE ( 'NONE', #49415, 3.400000000000000355 ) ;
#70792=DIRECTION ( 'NONE',  ( -0.8191520442889974607, 0.000000000000000000, -0.5735764363510379438 ) ) ;
#70808=EDGE_CURVE ( 'NONE', #26114, #83820, #41863, .T. ) ;
#70829=LINE ( 'NONE', #78909, #70707 ) ;
#70896=CARTESIAN_POINT ( 'NONE',  ( -2.055025722541619526, 6.319083845364129814, -5.720331885005969674 ) ) ;
#70916=ORIENTED_EDGE ( 'NONE', *, *, #1488, .T. ) ;
#70958=CARTESIAN_POINT ( 'NONE',  ( 6.500000000000000000, -3.155218591052682875, -0.5622968210053850280 ) ) ;
#70976=CARTESIAN_POINT ( 'NONE',  ( 0.000000000000000000, 0.000000000000000000, -4.987924522925830217 ) ) ;
#70986=DIRECTION ( 'NONE',  ( 0.000000000000000000, 0.000000000000000000, 1.000000000000000000 ) ) ;
#71065=ORIENTED_EDGE ( 'NONE', *, *, #31589, .T. ) ;
#71078=AXIS2_PLACEMENT_3D ( 'NONE', #25284, #59231, #17177 ) ;
#71103=VERTEX_POINT ( 'NONE', #13740 ) ;
#71110=DIRECTION ( 'NONE',  ( -0.8191520442889900222, 1.003171929053522528E-16, 0.5735764363510486019 ) ) ;
#71142=EDGE_CURVE ( 'NONE', #73863, #14310, #44711, .T. ) ;
#71177=CARTESIAN_POINT ( 'NONE',  ( -3.220999722221654600E-16, 7.895640089090876224, -6.564402953523721607 ) ) ;
#71187=ORIENTED_EDGE ( 'NONE', *, *, #8549, .F. ) ;
#71258=LINE ( 'NONE', #102578, #49339 ) ;
#71275=ORIENTED_EDGE ( 'NONE', *, *, #86149, .F. ) ;
#71293=CIRCLE ( 'NONE', #79758, 8.331345277524542681 ) ;
#71410=CARTESIAN_POINT ( 'NONE',  ( 0.2813450144774501949, 7.667988119308862593, -6.122077150241858057 ) ) ;
#71419=CARTESIAN_POINT ( 'NONE',  ( 3.400000000000000355, 0.000000000000000000, -4.147675477074182382 ) ) ;
#71442=DIRECTION ( 'NONE',  ( 0.000000000000000000, 0.000000000000000000, 1.000000000000000000 ) ) ;
#71467=DIRECTION ( 'NONE',  ( -1.000000000000000000, 0.000000000000000000, 0.000000000000000000 ) ) ;
#71468=ORIENTED_EDGE ( 'NONE', *, *, #3541, .F. ) ;
#71555=CARTESIAN_POINT ( 'NONE',  ( 0.000000000000000000, 0.000000000000000000, -8.000000000000000000 ) ) ;
#71585=AXIS2_PLACEMENT_3D ( 'NONE', #69197, #100475, #36329 ) ;
#71589=VERTEX_POINT ( 'NONE', #49155 ) ;
#71591=ORIENTED_EDGE ( 'NONE', *, *, #69165, .F. ) ;
#71685=VECTOR ( 'NONE', #61676, 1000.000000000000000 ) ;
#71710=CARTESIAN_POINT ( 'NONE',  ( -4.000000000000000000, 0.000000000000000000, -1.161000000000000032 ) ) ;
#71767=CARTESIAN_POINT ( 'NONE',  ( 2.971071886220384428, 5.790204346174069983, 1.217186345204429587E-15 ) ) ;
#71786=CIRCLE ( 'NONE', #13201, 3.400000000000000355 ) ;
#71864=ADVANCED_FACE ( 'NONE', ( #89391 ), #1717, .T. ) ;
#71995=ORIENTED_EDGE ( 'NONE', *, *, #67384, .T. ) ;
#71996=EDGE_CURVE ( 'NONE', #26262, #57008, #94167, .T. ) ;
#72013=VERTEX_POINT ( 'NONE', #10576 ) ;
#72056=VECTOR ( 'NONE', #45537, 1000.000000000000000 ) ;
#72195=EDGE_CURVE ( 'NONE', #14549, #76811, #56866, .T. ) ;
#72259=CARTESIAN_POINT ( 'NONE',  ( 5.193195059372482212E-16, -7.895640089090903757, -6.564402953523731377 ) ) ;
#72261=FACE_OUTER_BOUND ( 'NONE', #53484, .T. ) ;
#72274=DIRECTION ( 'NONE',  ( 0.000000000000000000, 0.000000000000000000, 1.000000000000000000 ) ) ;
#72315=CARTESIAN_POINT ( 'NONE',  ( 4.000000000000000000, 4.898587196589412829E-16, -6.838999999999999524 ) ) ;
#72422=ORIENTED_EDGE ( 'NONE', *, *, #83284, .F. ) ;
#72570=VERTEX_POINT ( 'NONE', #55148 ) ;
#72678=DIRECTION ( 'NONE',  ( 0.000000000000000000, 0.000000000000000000, 1.000000000000000000 ) ) ;
#72694=EDGE_LOOP ( 'NONE', ( #86346, #22531, #72422, #5134 ) ) ;
#72695=DIRECTION ( 'NONE',  ( -1.000000000000000000, 0.000000000000000000, 0.000000000000000000 ) ) ;
#72817=EDGE_CURVE ( 'NONE', #102355, #62903, #15570, .T. ) ;
#72818=EDGE_CURVE ( 'NONE', #59491, #14702, #16101, .T. ) ;
#72864=DIRECTION ( 'NONE',  ( -0.8660254037844373753, 0.5000000000000021094, 0.000000000000000000 ) ) ;
#73022=CARTESIAN_POINT ( 'NONE',  ( 0.000000000000000000, 0.000000000000000000, 3.469446951953614189E-15 ) ) ;
#73077=AXIS2_PLACEMENT_3D ( 'NONE', #89825, #24583, #48280 ) ;
#73100=ADVANCED_FACE ( 'NONE', ( #77755 ), #5965, .F. ) ;
#73103=B_SPLINE_CURVE_WITH_KNOTS ( 'NONE', 3,
 ( #5073, #88640, #40090, #38006, #55709 ),
 .UNSPECIFIED., .F., .F.,
 ( 4, 1, 4 ),
 ( 0.000000000000000000, 0.003752776749732572234, 0.007505553499465144468 ),
 .UNSPECIFIED. ) ;
#73197=FACE_OUTER_BOUND ( 'NONE', #2876, .T. ) ;
#73200=AXIS2_PLACEMENT_3D ( 'NONE', #68409, #75418, #58168 ) ;
#73308=CARTESIAN_POINT ( 'NONE',  ( -6.815830331203682313, 0.6610623347507927905, -6.171384342982605631 ) ) ;
#73362=CARTESIAN_POINT ( 'NONE',  ( 6.499999999999999112, 2.723353699433560315, -5.896365680526115760 ) ) ;
#73390=CARTESIAN_POINT ( 'NONE',  ( 0.000000000000000000, 0.000000000000000000, -5.703399999999999359 ) ) ;
#73398=ORIENTED_EDGE ( 'NONE', *, *, #53562, .T. ) ;
#73427=CARTESIAN_POINT ( 'NONE',  ( -3.809068165403739048, -5.306386968807679239, -1.794524002052960067E-14 ) ) ;
#73504=ADVANCED_FACE ( 'NONE', ( #44198 ), #103506, .T. ) ;
#73593=CARTESIAN_POINT ( 'NONE',  ( -3.400000000000000355, 4.163799117101001052E-16, -8.000000000000000000 ) ) ;
#73664=FACE_OUTER_BOUND ( 'NONE', #101086, .T. ) ;
#73735=EDGE_CURVE ( 'NONE', #95748, #112, #86795, .T. ) ;
#73779=DIRECTION ( 'NONE',  ( -0.000000000000000000, -0.000000000000000000, -1.000000000000000000 ) ) ;
#73810=VECTOR ( 'NONE', #1586, 1000.000000000000000 ) ;
#73817=ORIENTED_EDGE ( 'NONE', *, *, #46985, .F. ) ;
#73863=VERTEX_POINT ( 'NONE', #59201 ) ;
#73884=CARTESIAN_POINT ( 'NONE',  ( -3.400000000000000355, 4.163799117101001052E-16, -2.716724522925831220 ) ) ;
#73901=CARTESIAN_POINT ( 'NONE',  ( 6.499999999998793854, -1.392325603687970981, -6.058577540041909515 ) ) ;
#73922=EDGE_CURVE ( 'NONE', #48619, #102355, #75358, .T. ) ;
#74032=ADVANCED_FACE ( 'NONE', ( #49490 ), #371, .F. ) ;
#74042=CARTESIAN_POINT ( 'NONE',  ( 0.5219667817988785652, -7.204195837485550591, -0.5602453477493567480 ) ) ;
#74059=CARTESIAN_POINT ( 'NONE',  ( 1.381740507186689448E-16, 7.550813340387661832, -6.286444963328676749 ) ) ;
#74075=ORIENTED_EDGE ( 'NONE', *, *, #73922, .T. ) ;
#74138=DIRECTION ( 'NONE',  ( -0.000000000000000000, -0.000000000000000000, -1.000000000000000000 ) ) ;
#74154=ADVANCED_FACE ( 'NONE', ( #4147 ), #17433, .F. ) ;
#74181=AXIS2_PLACEMENT_3D ( 'NONE', #6883, #5821, #72678 ) ;
#74182=CARTESIAN_POINT ( 'NONE',  ( 5.007715329123895321E-16, -7.505553499465175804, -6.064240316920414209 ) ) ;
#74256=CARTESIAN_POINT ( 'NONE',  ( -3.400000000000000355, 4.163799117101001052E-16, -8.000000000000000000 ) ) ;
#74369=CARTESIAN_POINT ( 'NONE',  ( -6.139120788623333130E-13, -7.790635086498917339, -6.526184258131205951 ) ) ;
#74564=ORIENTED_EDGE ( 'NONE', *, *, #23670, .F. ) ;
#74585=EDGE_CURVE ( 'NONE', #29666, #35363, #33005, .T. ) ;
#74617=LINE ( 'NONE', #99415, #9683 ) ;
#74679=AXIS2_PLACEMENT_3D ( 'NONE', #61249, #45070, #77952 ) ;
#74698=VERTEX_POINT ( 'NONE', #26875 ) ;
#74725=EDGE_CURVE ( 'NONE', #39998, #28086, #43551, .T. ) ;
#74743=EDGE_CURVE ( 'NONE', #29175, #29666, #68212, .T. ) ;
#74773=ORIENTED_EDGE ( 'NONE', *, *, #99200, .F. ) ;
#74775=CARTESIAN_POINT ( 'NONE',  ( -4.000000000000002665, 0.000000000000000000, -7.974599999999995248 ) ) ;
#74788=EDGE_LOOP ( 'NONE', ( #20665, #4426, #53214, #6040 ) ) ;
#74814=EDGE_CURVE ( 'NONE', #80953, #100791, #8944, .T. ) ;
#74851=ORIENTED_EDGE ( 'NONE', *, *, #29868, .F. ) ;
#74967=AXIS2_PLACEMENT_3D ( 'NONE', #69326, #53655, #28351 ) ;
#75031=CARTESIAN_POINT ( 'NONE',  ( 8.542937654374686218, 1.046208125374535811E-15, -6.800000000000000711 ) ) ;
#75062=ORIENTED_EDGE ( 'NONE', *, *, #12136, .T. ) ;
#75071=CARTESIAN_POINT ( 'NONE',  ( 4.000000000000000000, 4.898587196589412829E-16, -4.567799999999999194 ) ) ;
#75083=EDGE_CURVE ( 'NONE', #50026, #80953, #38659, .T. ) ;
#75321=ORIENTED_EDGE ( 'NONE', *, *, #102673, .F. ) ;
#75332=ADVANCED_FACE ( 'NONE', ( #103257, #45037 ), #43954, .F. ) ;
#75358=LINE ( 'NONE', #1458, #91511 ) ;
#75397=AXIS2_PLACEMENT_3D ( 'NONE', #69310, #102186, #102726 ) ;
#75418=DIRECTION ( 'NONE',  ( -0.000000000000000000, -0.000000000000000000, -1.000000000000000000 ) ) ;
#75491=CYLINDRICAL_SURFACE ( 'NONE', #49723, 4.000000000000001776 ) ;
#75618=ORIENTED_EDGE ( 'NONE', *, *, #38803, .F. ) ;
#75666=EDGE_CURVE ( 'NONE', #9879, #83820, #8258, .T. ) ;
#75693=DIRECTION ( 'NONE',  ( 0.8660254037844372643, 0.5000000000000024425, 0.000000000000000000 ) ) ;
#75745=CARTESIAN_POINT ( 'NONE',  ( -6.499999999999999112, -1.360915494589017838, -5.718331000733962277 ) ) ;
#75749=CARTESIAN_POINT ( 'NONE',  ( 0.000000000000000000, 0.000000000000000000, -7.554475477074167777 ) ) ;
#75892=DIRECTION ( 'NONE',  ( -1.000000000000000000, 0.000000000000000000, 0.000000000000000000 ) ) ;
#75897=EDGE_CURVE ( 'NONE', #71589, #28086, #55079, .T. ) ;
#75985=VERTEX_POINT ( 'NONE', #7584 ) ;
#76024=DIRECTION ( 'NONE',  ( -1.000000000000000000, 0.000000000000000000, 0.000000000000000000 ) ) ;
#76146=CARTESIAN_POINT ( 'NONE',  ( 1.126429428730186588, -7.232124035235067083, -6.344710093416095376 ) ) ;
#76153=CONICAL_SURFACE ( 'NONE', #14164, 6.500000000000000888, 0.8987552595851637793 ) ;
#76177=DIRECTION ( 'NONE',  ( -0.000000000000000000, -0.000000000000000000, -1.000000000000000000 ) ) ;
#76195=EDGE_CURVE ( 'NONE', #74698, #3656, #56519, .T. ) ;
#76235=VERTEX_POINT ( 'NONE', #3240 ) ;
#76255=CARTESIAN_POINT ( 'NONE',  ( 6.500000000000000888, 0.000000000000000000, 1.734723475976807094E-15 ) ) ;
#76266=CARTESIAN_POINT ( 'NONE',  ( -4.000000000000000000, 0.000000000000000000, -5.703399999999999359 ) ) ;
#76349=DIRECTION ( 'NONE',  ( 0.8191520442889881348, 0.000000000000000000, 0.5735764363510513775 ) ) ;
#76375=ORIENTED_EDGE ( 'NONE', *, *, #105012, .F. ) ;
#76527=AXIS2_PLACEMENT_3D ( 'NONE', #23578, #56425, #81234 ) ;
#76572=CARTESIAN_POINT ( 'NONE',  ( -6.499999999999999112, -3.752776749732587902, -6.064240316920403551 ) ) ;
#76634=CARTESIAN_POINT ( 'NONE',  ( -6.837824896291514243, 3.947820044545419016, -6.564402953523714501 ) ) ;
#76802=CARTESIAN_POINT ( 'NONE',  ( -6.499999999999999112, 1.392044006195858774, -6.058542048163744198 ) ) ;
#76811=VERTEX_POINT ( 'NONE', #20099 ) ;
#76882=ORIENTED_EDGE ( 'NONE', *, *, #75083, .T. ) ;
#76896=EDGE_LOOP ( 'NONE', ( #55612, #63833, #38842, #58269, #40563 ) ) ;
#76954=SURFACE_SIDE_STYLE ('',( #103369 ) ) ;
#76959=CARTESIAN_POINT ( 'NONE',  ( 6.781345014477444977, 3.590342129888846046, -6.122077150241850063 ) ) ;
#76966=CARTESIAN_POINT ( 'NONE',  ( -1.058054217398702423, 6.894685612232783534, -0.3576316571898418006 ) ) ;
#76970=EDGE_CURVE ( 'NONE', #67283, #74698, #103618, .T. ) ;
#77073=ORIENTED_EDGE ( 'NONE', *, *, #50111, .F. ) ;
#77085=CARTESIAN_POINT ( 'NONE',  ( 0.000000000000000000, 0.000000000000000000, 1.734723475976807094E-15 ) ) ;
#77089=CONICAL_SURFACE ( 'NONE', #22065, 3.400000000000000355, 0.9599310885968748153 ) ;
#77517=CARTESIAN_POINT ( 'NONE',  ( -1.860380241283050795, -6.431462466365337249, -0.1499059597315451076 ) ) ;
#77755=FACE_OUTER_BOUND ( 'NONE', #95489, .T. ) ;
#77757=EDGE_LOOP ( 'NONE', ( #25448, #103027, #74075, #95886 ) ) ;
#77774=EDGE_CURVE ( 'NONE', #72013, #14549, #73103, .T. ) ;
#77862=B_SPLINE_CURVE_WITH_KNOTS ( 'NONE', 3,
 ( #9833, #92347, #41159, #60027, #74042, #67034 ),
 .UNSPECIFIED., .F., .F.,
 ( 4, 2, 4 ),
 ( 0.003841072314098320766, 0.005765657563962173389, 0.007690242813826025578 ),
 .UNSPECIFIED. ) ;
#77863=AXIS2_PLACEMENT_3D ( 'NONE', #36286, #5463, #28716 ) ;
#77873=ORIENTED_EDGE ( 'NONE', *, *, #42349, .F. ) ;
#77876=CARTESIAN_POINT ( 'NONE',  ( 0.000000000000000000, 0.000000000000000000, -6.800000000000000711 ) ) ;
#77891=ORIENTED_EDGE ( 'NONE', *, *, #35020, .F. ) ;
#77925=CARTESIAN_POINT ( 'NONE',  ( -2.241046694638763270, -6.576374040526363984, -6.171384342982626947 ) ) ;
#77929=CARTESIAN_POINT ( 'NONE',  ( -6.781345014477444089, 3.590342129888842049, -6.122077150241849175 ) ) ;
#77952=DIRECTION ( 'NONE',  ( 1.000000000000000000, 0.000000000000000000, 0.000000000000000000 ) ) ;
#78089=VECTOR ( 'NONE', #64612, 1000.000000000000000 ) ;
#78195=CARTESIAN_POINT ( 'NONE',  ( 6.499999999999999112, 3.752776749732559036, -6.064240316920397333 ) ) ;
#78244=CARTESIAN_POINT ( 'NONE',  ( 0.000000000000000000, 0.000000000000000000, -7.259124522925831435 ) ) ;
#78359=AXIS2_PLACEMENT_3D ( 'NONE', #56056, #54467, #79302 ) ;
#78396=CARTESIAN_POINT ( 'NONE',  ( -6.500000000000000000, 3.453380256388198788, -0.6809028088495666653 ) ) ;
#78474=DIRECTION ( 'NONE',  ( -0.000000000000000000, -0.000000000000000000, -1.000000000000000000 ) ) ;
#78540=CARTESIAN_POINT ( 'NONE',  ( 0.000000000000000000, 0.000000000000000000, -1.876475477074182940 ) ) ;
#78542=CARTESIAN_POINT ( 'NONE',  ( 0.000000000000000000, 0.000000000000000000, 0.000000000000000000 ) ) ;
#78743=ORIENTED_EDGE ( 'NONE', *, *, #67384, .F. ) ;
#78909=CARTESIAN_POINT ( 'NONE',  ( -3.400000000000000355, 4.163799117101001052E-16, -8.000000000000000000 ) ) ;
#78945=SURFACE_SIDE_STYLE ('',( #46063 ) ) ;
#78960=ORIENTED_EDGE ( 'NONE', *, *, #90201, .T. ) ;
#78981=CARTESIAN_POINT ( 'NONE',  ( 0.000000000000000000, 0.000000000000000000, -6.418875477074183600 ) ) ;
#79009=CARTESIAN_POINT ( 'NONE',  ( 0.000000000000000000, 0.000000000000000000, -4.147675477074182382 ) ) ;
#79086=CARTESIAN_POINT ( 'NONE',  ( 2.055025722541617750, 6.319083845364131591, -5.720331885005371930 ) ) ;
#79156=CARTESIAN_POINT ( 'NONE',  ( 0.000000000000000000, 0.000000000000000000, -5.283275477074182547 ) ) ;
#79181=EDGE_CURVE ( 'NONE', #15859, #70568, #34174, .T. ) ;
#79260=CARTESIAN_POINT ( 'NONE',  ( 6.837824896291514243, 3.947820044545422569, -6.564402953523715389 ) ) ;
#79302=DIRECTION ( 'NONE',  ( 1.000000000000000000, 0.000000000000000000, 0.000000000000000000 ) ) ;
#79340=ORIENTED_EDGE ( 'NONE', *, *, #100402, .F. ) ;
#79543=CARTESIAN_POINT ( 'NONE',  ( 0.000000000000000000, 0.000000000000000000, 0.000000000000000000 ) ) ;
#79607=DIRECTION ( 'NONE',  ( -0.000000000000000000, -0.000000000000000000, 1.000000000000000000 ) ) ;
#79654=ORIENTED_EDGE ( 'NONE', *, *, #94536, .F. ) ;
#79713=PLANE ( 'NONE',  #74181 ) ;
#79757=DIRECTION ( 'NONE',  ( 0.000000000000000000, 0.000000000000000000, -1.000000000000000000 ) ) ;
#79758=AXIS2_PLACEMENT_3D ( 'NONE', #5908, #96008, #13997 ) ;
#80125=DIRECTION ( 'NONE',  ( 0.8191520442889974607, 1.003171929053531649E-16, -0.5735764363510379438 ) ) ;
#80131=ADVANCED_FACE ( 'NONE', ( #73664 ), #61547, .F. ) ;
#80145=ORIENTED_EDGE ( 'NONE', *, *, #98938, .F. ) ;
#80179=DIRECTION ( 'NONE',  ( 1.000000000000000000, 0.000000000000000000, 0.000000000000000000 ) ) ;
#80240=CYLINDRICAL_SURFACE ( 'NONE', #52383, 3.400000000000000355 ) ;
#80253=EDGE_CURVE ( 'NONE', #86116, #75985, #5194, .T. ) ;
#80315=CARTESIAN_POINT ( 'NONE',  ( 0.5619217318086660029, 7.564468822943315018, -6.443866470201766283 ) ) ;
#80365=CONICAL_SURFACE ( 'NONE', #16709, 4.000000000000000000, 0.9599310885968912466 ) ;
#80399=CARTESIAN_POINT ( 'NONE',  ( 6.838249506730348592, 3.995160516047493893, -6.573190279698081007 ) ) ;
#80423=ADVANCED_FACE ( 'NONE', ( #35991 ), #63785, .F. ) ;
#80487=DIRECTION ( 'NONE',  ( 1.000000000000000000, 0.000000000000000000, 0.000000000000000000 ) ) ;
#80538=AXIS2_PLACEMENT_3D ( 'NONE', #103958, #46794, #87267 ) ;
#80563=ORIENTED_EDGE ( 'NONE', *, *, #94536, .T. ) ;
#80573=ORIENTED_EDGE ( 'NONE', *, *, #103617, .T. ) ;
#80692=CARTESIAN_POINT ( 'NONE',  ( 2.241046694639375669, -6.576374040525785780, -6.171384342982555893 ) ) ;
#80782=DIRECTION ( 'NONE',  ( 0.000000000000000000, 0.000000000000000000, 1.000000000000000000 ) ) ;
#80807=AXIS2_PLACEMENT_3D ( 'NONE', #66211, #7964, #81844 ) ;
#80831=CARTESIAN_POINT ( 'NONE',  ( -3.528928113779644438, 5.468125903023618228, 1.934623251528821186E-15 ) ) ;
#80906=EDGE_CURVE ( 'NONE', #88610, #82973, #81077, .T. ) ;
#80936=CARTESIAN_POINT ( 'NONE',  ( 6.499999999999999112, -4.076778466486165264, -6.121917890101378212 ) ) ;
#80947=LINE ( 'NONE', #7056, #101264 ) ;
#80953=VERTEX_POINT ( 'NONE', #76266 ) ;
#81077=CIRCLE ( 'NONE', #3576, 4.000000000000000000 ) ;
#81101=CARTESIAN_POINT ( 'NONE',  ( 3.250000000000015987, -5.629165124598843661, 1.734723475976807094E-15 ) ) ;
#81107=CARTESIAN_POINT ( 'NONE',  ( 4.000000000000000000, 4.898587196589412829E-16, -6.838999999999999524 ) ) ;
#81175=CARTESIAN_POINT ( 'NONE',  ( -6.499999999999999112, -3.752776749732587902, -6.064240316920403551 ) ) ;
#81234=DIRECTION ( 'NONE',  ( -1.000000000000000000, 0.000000000000000000, 0.000000000000000000 ) ) ;
#81249=CONICAL_SURFACE ( 'NONE', #91601, 3.400000000000000355, 0.9599310885968748153 ) ;
#81399=CARTESIAN_POINT ( 'NONE',  ( -6.815830331203684977, -1.215378054691643734E-13, -6.171384342982610072 ) ) ;
#81840=EDGE_CURVE ( 'NONE', #71103, #88610, #53862, .T. ) ;
#81844=DIRECTION ( 'NONE',  ( 0.8660254037844374864, -0.5000000000000019984, 0.000000000000000000 ) ) ;
#81928=DIRECTION ( 'NONE',  ( 1.000000000000000000, 0.000000000000000000, 0.000000000000000000 ) ) ;
#81988=CARTESIAN_POINT ( 'NONE',  ( 6.838238910409968341, -3.993980678889280878, -6.572970348078617242 ) ) ;
#82032=DIRECTION ( 'NONE',  ( -1.000000000000000000, 0.000000000000000000, 0.000000000000000000 ) ) ;
#82077=ORIENTED_EDGE ( 'NONE', *, *, #80906, .T. ) ;
#82144=B_SPLINE_CURVE_WITH_KNOTS ( 'NONE', 3,
 ( #91229, #25995, #34605, #92251, #66942, #58856 ),
 .UNSPECIFIED., .F., .F.,
 ( 4, 2, 4 ),
 ( 0.000000000000000000, 0.001990940508721421830, 0.003981881017442843659 ),
 .UNSPECIFIED. ) ;
#82164=DIRECTION ( 'NONE',  ( -0.000000000000000000, -0.000000000000000000, -1.000000000000000000 ) ) ;
#82216=B_SPLINE_CURVE_WITH_KNOTS ( 'NONE', 3,
 ( #65728, #99680, #25851, #47924, #98607, #25296, #80831, #31779 ),
 .UNSPECIFIED., .F., .F.,
 ( 4, 2, 2, 4 ),
 ( 2.459764730722484167E-07, 0.001920659145285706550, 0.002880865729692022332, 0.003841072314098338547 ),
 .UNSPECIFIED. ) ;
#82280=CARTESIAN_POINT ( 'NONE',  ( 1.083333333333333259, -6.880090707843076636, -5.848636054922048189 ) ) ;
#82370=ORIENTED_EDGE ( 'NONE', *, *, #29911, .T. ) ;
#82632=DIRECTION ( 'NONE',  ( -0.000000000000000000, -0.000000000000000000, 1.000000000000000000 ) ) ;
#82761=EDGE_CURVE ( 'NONE', #34748, #13321, #50281, .T. ) ;
#82931=ORIENTED_EDGE ( 'NONE', *, *, #95168, .T. ) ;
#82939=DIRECTION ( 'NONE',  ( 1.000000000000000000, 0.000000000000000000, 0.000000000000000000 ) ) ;
#82947=B_SPLINE_CURVE_WITH_KNOTS ( 'NONE', 3,
 ( #70197, #28715, #27662, #103105, #29254, #62135, #71767, #87983 ),
 .UNSPECIFIED., .F., .F.,
 ( 4, 2, 2, 4 ),
 ( 2.459764730735158427E-07, 0.001920659145285726066, 0.002880865729692052690, 0.003841072314098378879 ),
 .UNSPECIFIED. ) ;
#82973=VERTEX_POINT ( 'NONE', #72315 ) ;
#83064=DIRECTION ( 'NONE',  ( 0.000000000000000000, 0.000000000000000000, 1.000000000000000000 ) ) ;
#83075=DIRECTION ( 'NONE',  ( -0.000000000000000000, -0.000000000000000000, -1.000000000000000000 ) ) ;
#83076=ADVANCED_FACE ( 'NONE', ( #103498 ), #5343, .T. ) ;
#83102=DIRECTION ( 'NONE',  ( -0.000000000000000000, -0.000000000000000000, 1.000000000000000000 ) ) ;
#83251=DIRECTION ( 'NONE',  ( 0.000000000000000000, 0.000000000000000000, 1.000000000000000000 ) ) ;
#83284=EDGE_CURVE ( 'NONE', #75985, #86116, #29839, .T. ) ;
#83290=DIRECTION ( 'NONE',  ( -0.000000000000000000, -0.000000000000000000, -1.000000000000000000 ) ) ;
#83304=CARTESIAN_POINT ( 'NONE',  ( 6.500000000000000000, 3.453380256388234759, -0.6809028088495799880 ) ) ;
#83410=ORIENTED_EDGE ( 'NONE', *, *, #83284, .T. ) ;
#83623=FACE_OUTER_BOUND ( 'NONE', #23076, .T. ) ;
#83639=ORIENTED_EDGE ( 'NONE', *, *, #22779, .T. ) ;
#83665=ORIENTED_EDGE ( 'NONE', *, *, #15313, .T. ) ;
#83689=B_SPLINE_CURVE_WITH_KNOTS ( 'NONE', 3,
 ( #22681, #97059, #63660, #7502, #15079, #89514 ),
 .UNSPECIFIED., .F., .F.,
 ( 4, 2, 4 ),
 ( 0.000000000000000000, 0.001990940508721407518, 0.003981881017442815036 ),
 .UNSPECIFIED. ) ;
#83780=DIRECTION ( 'NONE',  ( 1.000000000000000000, 0.000000000000000000, 0.000000000000000000 ) ) ;
#83820=VERTEX_POINT ( 'NONE', #52554 ) ;
#83950=LINE ( 'NONE', #74256, #51508 ) ;
#83953=ADVANCED_FACE ( 'NONE', ( #55202 ), #24676, .F. ) ;
#83963=CARTESIAN_POINT ( 'NONE',  ( -3.400000000000000355, 4.163799117101001052E-16, -5.283275477074182547 ) ) ;
#84004=EDGE_CURVE ( 'NONE', #23499, #18245, #91319, .T. ) ;
#84125=LINE ( 'NONE', #87193, #73810 ) ;
#84178=ORIENTED_EDGE ( 'NONE', *, *, #49857, .F. ) ;
#84382=CARTESIAN_POINT ( 'NONE',  ( -6.499999999999999112, 4.076783350660889482, -6.121918786669028556 ) ) ;
#84487=ORIENTED_EDGE ( 'NONE', *, *, #56365, .F. ) ;
#84495=AXIS2_PLACEMENT_3D ( 'NONE', #35716, #27629, #93395 ) ;
#84511=AXIS2_PLACEMENT_3D ( 'NONE', #65186, #98080, #89993 ) ;
#84687=DIRECTION ( 'NONE',  ( -0.000000000000000000, -0.000000000000000000, -1.000000000000000000 ) ) ;
#84791=CYLINDRICAL_SURFACE ( 'NONE', #90349, 3.400000000000000355 ) ;
#84802=AXIS2_PLACEMENT_3D ( 'NONE', #46212, #103900, #13818 ) ;
#84867=CARTESIAN_POINT ( 'NONE',  ( 6.837824896291514243, 3.947820044545422569, -6.564402953523715389 ) ) ;
#84874=DIRECTION ( 'NONE',  ( 1.000000000000000000, 0.000000000000000000, 0.000000000000000000 ) ) ;
#84887=VERTEX_POINT ( 'NONE', #43576 ) ;
#84911=CARTESIAN_POINT ( 'NONE',  ( -6.838249472399976270, -3.995156693690935956, -6.573189567101946018 ) ) ;
#84969=( GEOMETRIC_REPRESENTATION_CONTEXT ( 3 ) GLOBAL_UNCERTAINTY_ASSIGNED_CONTEXT ( ( #65576 ) ) GLOBAL_UNIT_ASSIGNED_CONTEXT ( ( #85460, #13672, #44469 ) ) REPRESENTATION_CONTEXT ( 'NONE', 'WORKASPACE' ) );
#85011=CARTESIAN_POINT ( 'NONE',  ( 0.000000000000000000, 0.000000000000000000, 1.734723475976807094E-15 ) ) ;
#85040=ADVANCED_FACE ( 'NONE', ( #46762 ), #38689, .F. ) ;
#85045=ADVANCED_FACE ( 'NONE', ( #13316 ), #45535, .T. ) ;
#85046=DIRECTION ( 'NONE',  ( -1.000000000000000000, 0.000000000000000000, 0.000000000000000000 ) ) ;
#85049=EDGE_CURVE ( 'NONE', #95748, #18245, #95475, .T. ) ;
#85111=CIRCLE ( 'NONE', #38639, 3.400000000000000355 ) ;
#85268=CONICAL_SURFACE ( 'NONE', #64559, 3.400000000000000355, 0.9599310885968748153 ) ;
#85460=( LENGTH_UNIT ( ) NAMED_UNIT ( * ) SI_UNIT ( .MILLI., .METRE. ) );
#85538=CONICAL_SURFACE ( 'NONE', #1090, 3.400000000000000355, 0.9599310885968748153 ) ;
#85541=FACE_OUTER_BOUND ( 'NONE', #8953, .T. ) ;
#85622=CARTESIAN_POINT ( 'NONE',  ( -6.500000000000000888, 0.000000000000000000, 1.734723475976807094E-15 ) ) ;
#85674=ORIENTED_EDGE ( 'NONE', *, *, #90096, .F. ) ;
#85718=CIRCLE ( 'NONE', #68462, 3.400000000000000355 ) ;
#85761=CARTESIAN_POINT ( 'NONE',  ( 3.811597179862330709, -5.304926841629225898, -0.01956314070070098651 ) ) ;
#85787=DIRECTION ( 'NONE',  ( -0.000000000000000000, -0.000000000000000000, -1.000000000000000000 ) ) ;
#85813=CARTESIAN_POINT ( 'NONE',  ( 0.000000000000000000, 0.000000000000000000, -2.716724522925831220 ) ) ;
#85873=CARTESIAN_POINT ( 'NONE',  ( 6.818286579240214529, -1.325012739682879692, -6.208253321455268647 ) ) ;
#85945=FACE_OUTER_BOUND ( 'NONE', #18947, .T. ) ;
#86013=PRESENTATION_STYLE_ASSIGNMENT (( #54650 ) ) ;
#86082=EDGE_CURVE ( 'NONE', #88814, #88610, #6425, .T. ) ;
#86116=VERTEX_POINT ( 'NONE', #71710 ) ;
#86146=( NAMED_UNIT ( * ) PLANE_ANGLE_UNIT ( ) SI_UNIT ( $, .RADIAN. ) );
#86149=EDGE_CURVE ( 'NONE', #26262, #62903, #46401, .T. ) ;
#86157=EDGE_CURVE ( 'NONE', #38000, #25389, #83689, .T. ) ;
#86172=DIRECTION ( 'NONE',  ( -0.000000000000000000, -0.000000000000000000, -1.000000000000000000 ) ) ;
#86196=AXIS2_PLACEMENT_3D ( 'NONE', #1358, #60188, #100073 ) ;
#86314=AXIS2_PLACEMENT_3D ( 'NONE', #70976, #89291, #105976 ) ;
#86346=ORIENTED_EDGE ( 'NONE', *, *, #76195, .T. ) ;
#86452=B_SPLINE_CURVE_WITH_KNOTS ( 'NONE', 3,
 ( #31605, #8354, #64489, #88232, #105977, #81175 ),
 .UNSPECIFIED., .F., .F.,
 ( 4, 2, 4 ),
 ( -4.604908129294629295E-06, 0.0003318387708540386852, 0.0006682824498373720733 ),
 .UNSPECIFIED. ) ;
#86501=ORIENTED_EDGE ( 'NONE', *, *, #74585, .T. ) ;
#86507=CARTESIAN_POINT ( 'NONE',  ( -3.400000000000000355, 4.163799117101001052E-16, -8.000000000000000000 ) ) ;
#86620=DIRECTION ( 'NONE',  ( -0.000000000000000000, -0.000000000000000000, -1.000000000000000000 ) ) ;
#86674=CONICAL_SURFACE ( 'NONE', #45305, 3.400000000000000355, 0.9599310885968748153 ) ;
#86698=B_SPLINE_CURVE_WITH_KNOTS ( 'NONE', 3,
 ( #2542, #26869, #59739, #92616, #104419, #39180, #23005, #88781, #30035, #96357 ),
 .UNSPECIFIED., .F., .F.,
 ( 4, 2, 2, 2, 4 ),
 ( 0.000000000000000000, 0.001989602278884367460, 0.003979204557768734919, 0.005968806836653102812, 0.007958409115537469838 ),
 .UNSPECIFIED. ) ;
#86782=FACE_OUTER_BOUND ( 'NONE', #12538, .T. ) ;
#86795=LINE ( 'NONE', #28570, #1940 ) ;
#86807=EDGE_CURVE ( 'NONE', #5468, #30156, #25791, .T. ) ;
#86818=DIRECTION ( 'NONE',  ( 0.000000000000000000, 0.000000000000000000, 1.000000000000000000 ) ) ;
#86837=B_SPLINE_CURVE_WITH_KNOTS ( 'NONE', 3,
 ( #96123, #28776, #45456, #86981, #22786, #13585, #62187, #63761, #4447, #21206 ),
 .UNSPECIFIED., .F., .F.,
 ( 4, 2, 2, 2, 4 ),
 ( 1.909096309310500434E-19, 0.001989602278884367460, 0.003979204557768734919, 0.005968806836653102812, 0.007958409115537469838 ),
 .UNSPECIFIED. ) ;
#86844=ORIENTED_EDGE ( 'NONE', *, *, #2619, .T. ) ;
#86889=DIRECTION ( 'NONE',  ( 0.000000000000000000, 0.000000000000000000, 1.000000000000000000 ) ) ;
#86981=CARTESIAN_POINT ( 'NONE',  ( -2.262848203703083261, -6.566616684922180092, -6.208169345099799230 ) ) ;
#87043=ORIENTED_EDGE ( 'NONE', *, *, #75083, .F. ) ;
#87163=DIRECTION ( 'NONE',  ( 1.000000000000000000, 0.000000000000000000, 0.000000000000000000 ) ) ;
#87193=CARTESIAN_POINT ( 'NONE',  ( 3.400000000000000355, 0.000000000000000000, -8.000000000000000000 ) ) ;
#87267=DIRECTION ( 'NONE',  ( 1.000000000000000000, 0.000000000000000000, 0.000000000000000000 ) ) ;
#87353=ORIENTED_EDGE ( 'NONE', *, *, #70808, .F. ) ;
#87370=CARTESIAN_POINT ( 'NONE',  ( 6.663127973346358424, 3.846958729056439985, -6.460793508093575888 ) ) ;
#87375=EDGE_CURVE ( 'NONE', #9488, #10770, #82144, .T. ) ;
#87395=AXIS2_PLACEMENT_3D ( 'NONE', #31862, #56080, #31349 ) ;
#87412=FACE_OUTER_BOUND ( 'NONE', #25921, .T. ) ;
#87446=VECTOR ( 'NONE', #45616, 1000.000000000000000 ) ;
#87466=DIRECTION ( 'NONE',  ( 0.8191520442889974607, 1.003171929053531649E-16, -0.5735764363510379438 ) ) ;
#87472=CARTESIAN_POINT ( 'NONE',  ( 0.000000000000000000, 0.000000000000000000, -7.974599999999995248 ) ) ;
#87503=AXIS2_PLACEMENT_3D ( 'NONE', #33626, #42219, #35230 ) ;
#87563=CARTESIAN_POINT ( 'NONE',  ( 5.007715329123895321E-16, -7.505553499465175804, -8.000000000000000000 ) ) ;
#87585=EDGE_CURVE ( 'NONE', #31429, #48619, #95628, .T. ) ;
#87616=CARTESIAN_POINT ( 'NONE',  ( -2.075968632160923644, -6.306992450857648258, -6.056431503346049183 ) ) ;
#87690=ORIENTED_EDGE ( 'NONE', *, *, #33227, .F. ) ;
#87758=VERTEX_POINT ( 'NONE', #94533 ) ;
#87838=DIRECTION ( 'NONE',  ( -0.000000000000000000, -0.000000000000000000, -1.000000000000000000 ) ) ;
#87983=CARTESIAN_POINT ( 'NONE',  ( 3.250000000000015099, 5.629165124598843661, 1.734723475976807094E-15 ) ) ;
#88011=EDGE_CURVE ( 'NONE', #96068, #27489, #16385, .T. ) ;
#88149=FACE_OUTER_BOUND ( 'NONE', #91904, .T. ) ;
#88189=CARTESIAN_POINT ( 'NONE',  ( -3.400000000000000355, 4.163799117101001052E-16, -6.123524522925831270 ) ) ;
#88230=ORIENTED_EDGE ( 'NONE', *, *, #97905, .T. ) ;
#88232=CARTESIAN_POINT ( 'NONE',  ( -6.539196172010136365, -3.775406670193843794, -6.286444963328675861 ) ) ;
#88246=EDGE_CURVE ( 'NONE', #40596, #84887, #42510, .T. ) ;
#88266=CONICAL_SURFACE ( 'NONE', #21092, 6.500000000000000888, 0.8987552595851637793 ) ;
#88298=VECTOR ( 'NONE', #28838, 1000.000000000000000 ) ;
#88438=DIRECTION ( 'NONE',  ( -0.8191520442889881348, 1.003171929053520186E-16, 0.5735764363510513775 ) ) ;
#88510=CIRCLE ( 'NONE', #64493, 3.400000000000000355 ) ;
#88527=ORIENTED_EDGE ( 'NONE', *, *, #82761, .T. ) ;
#88531=ADVANCED_FACE ( 'NONE', ( #102652 ), #35599, .F. ) ;
#88598=CARTESIAN_POINT ( 'NONE',  ( 6.663127973346361976, -3.846958729056464410, -6.460793508093581217 ) ) ;
#88610=VERTEX_POINT ( 'NONE', #8049 ) ;
#88640=CARTESIAN_POINT ( 'NONE',  ( -6.500000000000000000, 2.501851166488365585, -5.848636054922033978 ) ) ;
#88671=ADVANCED_FACE ( 'NONE', ( #59283 ), #67373, .F. ) ;
#88681=CONICAL_SURFACE ( 'NONE', #78359, 3.400000000000000355, 0.9599310885968748153 ) ;
#88735=DIRECTION ( 'NONE',  ( 0.000000000000000000, 0.000000000000000000, 1.000000000000000000 ) ) ;
#88751=EDGE_LOOP ( 'NONE', ( #104738, #55635, #39542, #35751 ) ) ;
#88781=CARTESIAN_POINT ( 'NONE',  ( -1.126429428730187476, 7.232124035235039550, -6.344710093416086494 ) ) ;
#88814=VERTEX_POINT ( 'NONE', #93664 ) ;
#88873=ORIENTED_EDGE ( 'NONE', *, *, #71996, .T. ) ;
#88949=ORIENTED_EDGE ( 'NONE', *, *, #51196, .T. ) ;
#88994=FACE_OUTER_BOUND ( 'NONE', #3561, .T. ) ;
#88998=ADVANCED_FACE ( 'NONE', ( #32663 ), #97514, .F. ) ;
#89221=CIRCLE ( 'NONE', #103002, 4.000000000000000888 ) ;
#89265=ORIENTED_EDGE ( 'NONE', *, *, #1488, .F. ) ;
#89291=DIRECTION ( 'NONE',  ( -0.000000000000000000, -0.000000000000000000, -1.000000000000000000 ) ) ;
#89391=FACE_OUTER_BOUND ( 'NONE', #29092, .T. ) ;
#89404=ORIENTED_EDGE ( 'NONE', *, *, #82761, .F. ) ;
#89514=CARTESIAN_POINT ( 'NONE',  ( 6.815830331203684977, 1.210606185736183200E-13, -6.171384342982610072 ) ) ;
#89524=ORIENTED_EDGE ( 'NONE', *, *, #7549, .F. ) ;
#89582=VECTOR ( 'NONE', #20335, 1000.000000000000000 ) ;
#89662=CARTESIAN_POINT ( 'NONE',  ( -4.000000000000000000, 0.000000000000000000, -0.02540000000000007530 ) ) ;
#89686=CIRCLE ( 'NONE', #103456, 4.000000000000000000 ) ;
#89786=LINE ( 'NONE', #48767, #60744 ) ;
#89825=CARTESIAN_POINT ( 'NONE',  ( 0.000000000000000000, 0.000000000000000000, -2.296599999999999753 ) ) ;
#89844=DIRECTION ( 'NONE',  ( 1.000000000000000000, 0.000000000000000000, 0.000000000000000000 ) ) ;
#89993=DIRECTION ( 'NONE',  ( -1.000000000000000000, 0.000000000000000000, 0.000000000000000000 ) ) ;
#90041=CARTESIAN_POINT ( 'NONE',  ( -6.826425371444816648, 2.641426549045764016, -6.344843397090114578 ) ) ;
#90049=CARTESIAN_POINT ( 'NONE',  ( 0.000000000000000000, 0.000000000000000000, -5.703399999999999359 ) ) ;
#90096=EDGE_CURVE ( 'NONE', #54633, #29666, #36059, .T. ) ;
#90129=DIRECTION ( 'NONE',  ( -0.000000000000000000, -0.000000000000000000, -1.000000000000000000 ) ) ;
#90182=EDGE_CURVE ( 'NONE', #37530, #46925, #63975, .T. ) ;
#90201=EDGE_CURVE ( 'NONE', #34748, #14310, #63450, .T. ) ;
#90334=DIRECTION ( 'NONE',  ( -1.000000000000000000, 0.000000000000000000, 0.000000000000000000 ) ) ;
#90349=AXIS2_PLACEMENT_3D ( 'NONE', #24980, #42733, #33597 ) ;
#90506=CARTESIAN_POINT ( 'NONE',  ( 0.000000000000000000, 0.000000000000000000, -0.02540000000000007530 ) ) ;
#90519=ADVANCED_FACE ( 'NONE', ( #103626 ), #31747, .T. ) ;
#90617=AXIS2_PLACEMENT_3D ( 'NONE', #18854, #26945, #43093 ) ;
#90633=FACE_OUTER_BOUND ( 'NONE', #96776, .T. ) ;
#90667=CIRCLE ( 'NONE', #52791, 4.000000000000000000 ) ;
#90954=ORIENTED_EDGE ( 'NONE', *, *, #51196, .F. ) ;
#90957=DIRECTION ( 'NONE',  ( 0.000000000000000000, 0.000000000000000000, 1.000000000000000000 ) ) ;
#91023=CARTESIAN_POINT ( 'NONE',  ( -3.400000000000000355, 4.163799117101001052E-16, -8.000000000000000000 ) ) ;
#91038=CARTESIAN_POINT ( 'NONE',  ( -3.400000000000000355, 4.163799117101001052E-16, -0.7408754770741831086 ) ) ;
#91103=CARTESIAN_POINT ( 'NONE',  ( 6.837824896291514243, 3.947820044545422569, -6.564402953523715389 ) ) ;
#91120=AXIS2_PLACEMENT_3D ( 'NONE', #14687, #96696, #63808 ) ;
#91122=CARTESIAN_POINT ( 'NONE',  ( 2.785715769379251079E-15, -7.693917458112937702, -6.460793508093594539 ) ) ;
#91168=AXIS2_PLACEMENT_3D ( 'NONE', #10898, #76177, #44359 ) ;
#91229=CARTESIAN_POINT ( 'NONE',  ( -6.837824896291513355, -3.947820044545450102, -6.564402953523720718 ) ) ;
#91292=AXIS2_PLACEMENT_3D ( 'NONE', #61544, #29207, #36759 ) ;
#91308=CARTESIAN_POINT ( 'NONE',  ( -6.499999999999999112, -3.752776749732595452, -0.7999999999999977129 ) ) ;
#91319=LINE ( 'NONE', #40100, #33295 ) ;
#91341=EDGE_LOOP ( 'NONE', ( #19878, #19953, #58710, #6874 ) ) ;
#91377=EDGE_LOOP ( 'NONE', ( #15046, #63542 ) ) ;
#91417=CARTESIAN_POINT ( 'NONE',  ( 6.499999999999999112, 0.6470732608156867238, -0.01945970098672831355 ) ) ;
#91480=EDGE_CURVE ( 'NONE', #35363, #29175, #77862, .T. ) ;
#91511=VECTOR ( 'NONE', #2533, 1000.000000000000000 ) ;
#91543=EDGE_LOOP ( 'NONE', ( #80573, #56299, #11515, #18223 ) ) ;
#91601=AXIS2_PLACEMENT_3D ( 'NONE', #52337, #2724, #42656 ) ;
#91619=ORIENTED_EDGE ( 'NONE', *, *, #88246, .T. ) ;
#91636=ORIENTED_EDGE ( 'NONE', *, *, #74814, .T. ) ;
#91859=CONICAL_SURFACE ( 'NONE', #74679, 3.400000000000000355, 0.9599310885968748153 ) ;
#91903=ADVANCED_FACE ( 'NONE', ( #24346 ), #19122, .F. ) ;
#91904=EDGE_LOOP ( 'NONE', ( #28416, #90954, #1500, #29687 ) ) ;
#91916=CARTESIAN_POINT ( 'NONE',  ( 0.000000000000000000, 0.000000000000000000, -0.4455245229258316120 ) ) ;
#91953=EDGE_CURVE ( 'NONE', #46925, #94099, #89686, .T. ) ;
#91957=DIRECTION ( 'NONE',  ( 0.000000000000000000, 0.000000000000000000, -1.000000000000000000 ) ) ;
#92110=ORIENTED_EDGE ( 'NONE', *, *, #12136, .F. ) ;
#92132=AXIS2_PLACEMENT_3D ( 'NONE', #78244, #86889, #62092 ) ;
#92251=CARTESIAN_POINT ( 'NONE',  ( -6.818272094961328023, -1.321852500971161248, -6.208027553811809263 ) ) ;
#92299=AXIS2_PLACEMENT_3D ( 'NONE', #48352, #65078, #97976 ) ;
#92342=CARTESIAN_POINT ( 'NONE',  ( -6.499999999999999112, -1.280811194704867262, -0.07768058122908140517 ) ) ;
#92346=CYLINDRICAL_SURFACE ( 'NONE', #44002, 3.400000000000000355 ) ;
#92347=CARTESIAN_POINT ( 'NONE',  ( 2.690931834596300476, -5.951943280390056934, -1.764030815951805255E-14 ) ) ;
#92356=ADVANCED_BREP_SHAPE_REPRESENTATION ( '', ( #17340, #10728 ), #3983 ) ;
#92403=CARTESIAN_POINT ( 'NONE',  ( 5.007715329123895321E-16, -7.505553499465175804, -8.000000000000000000 ) ) ;
#92458=DIRECTION ( 'NONE',  ( -0.000000000000000000, -0.000000000000000000, 1.000000000000000000 ) ) ;
#92563=FACE_OUTER_BOUND ( 'NONE', #3817, .T. ) ;
#92594=CIRCLE ( 'NONE', #30644, 8.331345277524542681 ) ;
#92616=CARTESIAN_POINT ( 'NONE',  ( -4.555432764205793461, 5.242992371775925697, -6.208169345099787684 ) ) ;
#92762=CARTESIAN_POINT ( 'NONE',  ( 4.639619758717001829, -4.826867782832391818, -0.1499059597315433867 ) ) ;
#92865=CARTESIAN_POINT ( 'NONE',  ( 6.270061300899935297, -4.268872906156522262, -6.443866470201764507 ) ) ;
#92912=ORIENTED_EDGE ( 'NONE', *, *, #72195, .F. ) ;
#92996=CARTESIAN_POINT ( 'NONE',  ( -6.826296012759263121, -2.664253980648909614, -6.325071479459888124 ) ) ;
#93005=ORIENTED_EDGE ( 'NONE', *, *, #91953, .T. ) ;
#93021=EDGE_CURVE ( 'NONE', #18245, #14702, #12419, .T. ) ;
#93112=AXIS2_PLACEMENT_3D ( 'NONE', #46026, #12571, #38999 ) ;
#93134=VECTOR ( 'NONE', #48349, 1000.000000000000000 ) ;
#93262=EDGE_CURVE ( 'NONE', #76235, #26529, #22272, .T. ) ;
#93288=CARTESIAN_POINT ( 'NONE',  ( 0.000000000000000000, 0.000000000000000000, -5.283275477074182547 ) ) ;
#93395=DIRECTION ( 'NONE',  ( 1.000000000000000000, 0.000000000000000000, 0.000000000000000000 ) ) ;
#93545=CARTESIAN_POINT ( 'NONE',  ( -6.499999999999998224, 4.012863338656268652, -6.470131626772280597 ) ) ;
#93624=CARTESIAN_POINT ( 'NONE',  ( 3.400000000000000355, 0.000000000000000000, -6.123524522925831270 ) ) ;
#93660=CARTESIAN_POINT ( 'NONE',  ( 3.400000000000000355, 0.000000000000000000, -5.283275477074182547 ) ) ;
#93661=CARTESIAN_POINT ( 'NONE',  ( 0.000000000000000000, 0.000000000000000000, -0.4621369752184079083 ) ) ;
#93664=CARTESIAN_POINT ( 'NONE',  ( -3.400000000000000355, 4.163799117101001052E-16, -7.259124522925831435 ) ) ;
#93699=EDGE_CURVE ( 'NONE', #30156, #82973, #89786, .T. ) ;
#93703=AXIS2_PLACEMENT_3D ( 'NONE', #85813, #18420, #18970 ) ;
#93710=CARTESIAN_POINT ( 'NONE',  ( -3.400000000000000355, 4.163799117101001052E-16, -7.554475477074167777 ) ) ;
#93714=AXIS2_PLACEMENT_3D ( 'NONE', #31667, #7351, #6284 ) ;
#93850=B_SPLINE_CURVE_WITH_KNOTS ( 'NONE', 3,
 ( #23180, #15054, #40398, #57624, #32338 ),
 .UNSPECIFIED., .F., .F.,
 ( 4, 1, 4 ),
 ( 0.000000000000000000, 0.003752776749732572668, 0.007505553499465145335 ),
 .UNSPECIFIED. ) ;
#93857=DIRECTION ( 'NONE',  ( -1.000000000000000000, 0.000000000000000000, 0.000000000000000000 ) ) ;
#93899=EDGE_CURVE ( 'NONE', #87758, #11437, #56999, .T. ) ;
#93982=FACE_OUTER_BOUND ( 'NONE', #91543, .T. ) ;
#94010=ORIENTED_EDGE ( 'NONE', *, *, #86082, .F. ) ;
#94069=B_SPLINE_CURVE_WITH_KNOTS ( 'NONE', 3,
 ( #60008, #92865, #62131, #28711, #36281, #3337, #37334, #76146, #103101, #51870 ),
 .UNSPECIFIED., .F., .F.,
 ( 4, 2, 2, 2, 4 ),
 ( 0.000000000000000000, 0.001989602278884367460, 0.003979204557768734919, 0.005968806836653102812, 0.007958409115537469838 ),
 .UNSPECIFIED. ) ;
#94093=EDGE_LOOP ( 'NONE', ( #77073, #28768, #100822, #56277, #46371 ) ) ;
#94099=VERTEX_POINT ( 'NONE', #89662 ) ;
#94105=PRODUCT ( 'hex flange nut_din_Hexagon Flange Nut DIN 6923 - M8 - S', 'hex flange nut_din_Hexagon Flange Nut DIN 6923 - M8 - S', '', ( #97263 ) ) ;
#94167=LINE ( 'NONE', #18712, #89582 ) ;
#94184=CARTESIAN_POINT ( 'NONE',  ( 6.499999999999999112, -1.280811194704862377, -0.07768058122908151619 ) ) ;
#94208=DIRECTION ( 'NONE',  ( -0.000000000000000000, -0.000000000000000000, -1.000000000000000000 ) ) ;
#94220=CARTESIAN_POINT ( 'NONE',  ( -0.2259792476677689177, 7.636022678937404606, -6.470294263593365791 ) ) ;
#94377=CARTESIAN_POINT ( 'NONE',  ( 5.450967621166023847, -4.358435876041018453, -0.3607371497494629708 ) ) ;
#94432=AXIS2_PLACEMENT_3D ( 'NONE', #90049, #97589, #31834 ) ;
#94483=DIRECTION ( 'NONE',  ( 1.000000000000000000, 0.000000000000000000, 0.000000000000000000 ) ) ;
#94533=CARTESIAN_POINT ( 'NONE',  ( 6.499999999999999112, -3.752776749732586126, -6.064240316920402663 ) ) ;
#94536=EDGE_CURVE ( 'NONE', #9488, #14549, #86452, .T. ) ;
#94607=LINE ( 'NONE', #87563, #88298 ) ;
#94655=VERTEX_POINT ( 'NONE', #68602 ) ;
#94665=CARTESIAN_POINT ( 'NONE',  ( -6.725979247667767780, 3.622307570260298704, -6.470294263593356909 ) ) ;
#94872=DIRECTION ( 'NONE',  ( 1.000000000000000000, 0.000000000000000000, 0.000000000000000000 ) ) ;
#95003=B_SPLINE_CURVE_WITH_KNOTS ( 'NONE', 3,
 ( #49793, #97810, #6679, #74059, #64407, #97280 ),
 .UNSPECIFIED., .F., .F.,
 ( 4, 2, 4 ),
 ( -4.604908129295353508E-06, 0.0003318387708540403657, 0.0006682824498373760849 ),
 .UNSPECIFIED. ) ;
#95110=CARTESIAN_POINT ( 'NONE',  ( 6.539198257602121700, -3.775407874310934719, -6.286450516131051991 ) ) ;
#95168=EDGE_CURVE ( 'NONE', #37530, #102954, #105599, .T. ) ;
#95179=CARTESIAN_POINT ( 'NONE',  ( -5.589124336233769696, -4.278671059403218457, -6.219623095963493498 ) ) ;
#95199=EDGE_LOOP ( 'NONE', ( #68761, #70916, #18142, #55114 ) ) ;
#95297=CARTESIAN_POINT ( 'NONE',  ( -2.971071886220395530, -5.790204346174092187, -1.819539708428537912E-14 ) ) ;
#95322=DIRECTION ( 'NONE',  ( 1.000000000000000000, 0.000000000000000000, -0.000000000000000000 ) ) ;
#95351=DIRECTION ( 'NONE',  ( -1.000000000000000000, 0.000000000000000000, 0.000000000000000000 ) ) ;
#95475=CIRCLE ( 'NONE', #93714, 3.400000000000000355 ) ;
#95489=EDGE_LOOP ( 'NONE', ( #97283, #101028, #78960, #69280 ) ) ;
#95539=EDGE_CURVE ( 'NONE', #25389, #11437, #38672, .T. ) ;
#95545=EDGE_CURVE ( 'NONE', #11437, #26529, #94069, .T. ) ;
#95559=CIRCLE ( 'NONE', #5998, 3.400000000000000355 ) ;
#95576=CARTESIAN_POINT ( 'NONE',  ( 5.978033218201109555, 4.054134411712192687, -0.5602453477493177791 ) ) ;
#95577=CARTESIAN_POINT ( 'NONE',  ( 0.000000000000000000, 0.000000000000000000, -8.000000000000000000 ) ) ;
#95628=CIRCLE ( 'NONE', #98979, 3.400000000000000355 ) ;
#95654=CARTESIAN_POINT ( 'NONE',  ( -6.500000000000000888, 0.000000000000000000, 1.734723475976807094E-15 ) ) ;
#95734=DIRECTION ( 'NONE',  ( 0.000000000000000000, 0.000000000000000000, 1.000000000000000000 ) ) ;
#95748=VERTEX_POINT ( 'NONE', #58244 ) ;
#95826=CARTESIAN_POINT ( 'NONE',  ( -2.688402820137723914, -5.953403407568504946, -0.01956314070070124325 ) ) ;
#95866=AXIS2_PLACEMENT_3D ( 'NONE', #78981, #38546, #14231 ) ;
#95886=ORIENTED_EDGE ( 'NONE', *, *, #40212, .F. ) ;
#95944=CARTESIAN_POINT ( 'NONE',  ( -3.400000000000000355, 4.163799117101001052E-16, -6.123524522925831270 ) ) ;
#96008=DIRECTION ( 'NONE',  ( -0.000000000000000000, -0.000000000000000000, 1.000000000000000000 ) ) ;
#96022=AXIS2_PLACEMENT_3D ( 'NONE', #103278, #44518, #37518 ) ;
#96032=EDGE_CURVE ( 'NONE', #10770, #5773, #105093, .T. ) ;
#96068=VERTEX_POINT ( 'NONE', #95944 ) ;
#96123=CARTESIAN_POINT ( 'NONE',  ( 5.193195059372482212E-16, -7.895640089090903757, -6.564402953523731377 ) ) ;
#96263=CARTESIAN_POINT ( 'NONE',  ( 0.000000000000000000, 0.000000000000000000, -1.876475477074182940 ) ) ;
#96319=ORIENTED_EDGE ( 'NONE', *, *, #7549, .T. ) ;
#96357=CARTESIAN_POINT ( 'NONE',  ( -3.220999722221654600E-16, 7.895640089090876224, -6.564402953523721607 ) ) ;
#96379=VERTEX_POINT ( 'NONE', #40097 ) ;
#96385=CARTESIAN_POINT ( 'NONE',  ( 0.000000000000000000, 0.000000000000000000, -4.567799999999999194 ) ) ;
#96510=VECTOR ( 'NONE', #36275, 1000.000000000000114 ) ;
#96560=ORIENTED_EDGE ( 'NONE', *, *, #3541, .T. ) ;
#96609=CARTESIAN_POINT ( 'NONE',  ( 6.499999999999403144, 1.333904739168199960, -6.094327662196310946 ) ) ;
#96628=ADVANCED_FACE ( 'NONE', ( #57063 ), #60809, .T. ) ;
#96696=DIRECTION ( 'NONE',  ( -0.000000000000000000, -0.000000000000000000, -1.000000000000000000 ) ) ;
#96768=CARTESIAN_POINT ( 'NONE',  ( 0.000000000000000000, 0.000000000000000000, 0.000000000000000000 ) ) ;
#96776=EDGE_LOOP ( 'NONE', ( #24424, #62056, #13124, #2499, #41773 ) ) ;
#96851=EDGE_CURVE ( 'NONE', #50026, #95748, #40705, .T. ) ;
#96852=AXIS2_PLACEMENT_3D ( 'NONE', #28761, #52992, #62170 ) ;
#96879=CARTESIAN_POINT ( 'NONE',  ( -4.000000000000000000, 0.000000000000000000, -5.703399999999999359 ) ) ;
#97059=CARTESIAN_POINT ( 'NONE',  ( 6.831979103402614051, 3.295157223185828155, -6.443785395948805395 ) ) ;
#97066=CARTESIAN_POINT ( 'NONE',  ( 0.000000000000000000, 0.000000000000000000, -1.581124522925831499 ) ) ;
#97073=CYLINDRICAL_SURFACE ( 'NONE', #27328, 3.400000000000000355 ) ;
#97122=VECTOR ( 'NONE', #487, 1000.000000000000000 ) ;
#97141=ORIENTED_EDGE ( 'NONE', *, *, #100772, .T. ) ;
#97204=CARTESIAN_POINT ( 'NONE',  ( 6.746887896522141936, -3.895317543249906755, -6.526184258131190852 ) ) ;
#97249=EDGE_LOOP ( 'NONE', ( #88527, #23028, #5675, #21137 ) ) ;
#97255=EDGE_CURVE ( 'NONE', #37427, #5773, #98800, .T. ) ;
#97263=PRODUCT_CONTEXT ( 'NONE', #16230, 'mechanical' ) ;
#97280=CARTESIAN_POINT ( 'NONE',  ( -2.352990130084491319E-16, 7.505553499465148271, -6.064240316920404439 ) ) ;
#97283=ORIENTED_EDGE ( 'NONE', *, *, #49698, .F. ) ;
#97417=DIRECTION ( 'NONE',  ( 0.000000000000000000, 0.000000000000000000, 1.000000000000000000 ) ) ;
#97481=CARTESIAN_POINT ( 'NONE',  ( 3.400000000000000355, 0.000000000000000000, -8.000000000000000000 ) ) ;
#97514=CONICAL_SURFACE ( 'NONE', #11368, 4.000000000000000000, 0.9599310885968912466 ) ;
#97530=ADVANCED_FACE ( 'NONE', ( #86782 ), #80240, .F. ) ;
#97577=CARTESIAN_POINT ( 'NONE',  ( 0.000000000000000000, 0.000000000000000000, -8.000000000000000000 ) ) ;
#97589=DIRECTION ( 'NONE',  ( -0.000000000000000000, -0.000000000000000000, -1.000000000000000000 ) ) ;
#97654=B_SPLINE_CURVE_WITH_KNOTS ( 'NONE', 3,
 ( #71177, #80315, #63099, #39365, #64173, #23184, #15058, #100756, #9613, #91103 ),
 .UNSPECIFIED., .F., .F.,
 ( 4, 2, 2, 2, 4 ),
 ( 1.155223362816825029E-19, 0.001989602278884367026, 0.003979204557768734052, 0.005968806836653101078, 0.007958409115537469838 ),
 .UNSPECIFIED. ) ;
#97656=CARTESIAN_POINT ( 'NONE',  ( 5.416666666666665186, 4.378239541354655984, -5.848636054922034866 ) ) ;
#97663=ADVANCED_FACE ( 'NONE', ( #44603 ), #9541, .F. ) ;
#97784=CIRCLE ( 'NONE', #65072, 3.400000000000000355 ) ;
#97810=CARTESIAN_POINT ( 'NONE',  ( 7.760110535507928807E-13, 7.790254909845448772, -6.526045885145578040 ) ) ;
#97905=EDGE_CURVE ( 'NONE', #67283, #17532, #85111, .T. ) ;
#97907=B_SPLINE_CURVE_WITH_KNOTS ( 'NONE', 3,
 ( #32269, #65144, #31227, #31741, #106657 ),
 .UNSPECIFIED., .F., .F.,
 ( 4, 1, 4 ),
 ( 0.000000000000000000, 0.003752776749732572668, 0.007505553499465145335 ),
 .UNSPECIFIED. ) ;
#97969=LINE ( 'NONE', #17066, #66603 ) ;
#97976=DIRECTION ( 'NONE',  ( -1.000000000000000000, 0.000000000000000000, 0.000000000000000000 ) ) ;
#97978=ADVANCED_FACE ( 'NONE', ( #65012 ), #14562, .F. ) ;
#98000=EDGE_LOOP ( 'NONE', ( #102998, #29440, #61459, #82077 ) ) ;
#98025=DIRECTION ( 'NONE',  ( -0.000000000000000000, -0.000000000000000000, -1.000000000000000000 ) ) ;
#98076=ADVANCED_FACE ( 'NONE', ( #17411 ), #84791, .F. ) ;
#98080=DIRECTION ( 'NONE',  ( -0.000000000000000000, -0.000000000000000000, -1.000000000000000000 ) ) ;
#98123=CARTESIAN_POINT ( 'NONE',  ( 5.007715329123898279E-16, -7.505553499465175804, -6.177805531629075197 ) ) ;
#98184=CARTESIAN_POINT ( 'NONE',  ( 6.500000000000597744, 2.679956093905103920, -6.238387772031950718 ) ) ;
#98222=LINE ( 'NONE', #58850, #37149 ) ;
#98327=CARTESIAN_POINT ( 'NONE',  ( 4.000000000000000000, 4.898587196589412829E-16, -1.161000000000000032 ) ) ;
#98338=ORIENTED_EDGE ( 'NONE', *, *, #45609, .T. ) ;
#98343=EDGE_CURVE ( 'NONE', #25185, #18921, #82947, .T. ) ;
#98403=ORIENTED_EDGE ( 'NONE', *, *, #95539, .T. ) ;
#98460=CARTESIAN_POINT ( 'NONE',  ( 3.250000000000002220, -5.629165124598879189, -5.592027715088716988 ) ) ;
#98473=CARTESIAN_POINT ( 'NONE',  ( 2.055025722542327404, -6.319083845363749674, -5.720331885005380812 ) ) ;
#98495=EDGE_LOOP ( 'NONE', ( #88230, #83639, #45691, #62443 ) ) ;
#98588=ADVANCED_FACE ( 'NONE', ( #17283 ), #85268, .F. ) ;
#98607=CARTESIAN_POINT ( 'NONE',  ( -4.366061277241459315, 4.984806845751375448, -0.09463688534106240446 ) ) ;
#98711=MECHANICAL_DESIGN_GEOMETRIC_PRESENTATION_REPRESENTATION('',(#14569),#26480);
#98729=CARTESIAN_POINT ( 'NONE',  ( 6.499999999999999112, 3.752776749732559036, -8.000000000000000000 ) ) ;
#98766=CARTESIAN_POINT ( 'NONE',  ( -3.250000000000013767, -5.629165124598844550, 1.734723475976807094E-15 ) ) ;
#98800=CIRCLE ( 'NONE', #62654, 8.542937654374686218 ) ;
#98914=DIRECTION ( 'NONE',  ( 0.8191520442889974607, 1.003171929053531649E-16, -0.5735764363510379438 ) ) ;
#98938=EDGE_CURVE ( 'NONE', #48619, #31429, #57676, .T. ) ;
#98968=CARTESIAN_POINT ( 'NONE',  ( -6.499999999999999112, 3.752776749732556816, -0.7999999999999821698 ) ) ;
#98979=AXIS2_PLACEMENT_3D ( 'NONE', #10280, #2177, #82032 ) ;
#98994=CARTESIAN_POINT ( 'NONE',  ( 6.878751942472529635, -3.924677726130942457, -6.573129608219093534 ) ) ;
#99105=CARTESIAN_POINT ( 'NONE',  ( 0.000000000000000000, 0.000000000000000000, 0.000000000000000000 ) ) ;
#99120=DIRECTION ( 'NONE',  ( -1.000000000000000000, 0.000000000000000000, 0.000000000000000000 ) ) ;
#99182=ORIENTED_EDGE ( 'NONE', *, *, #6595, .T. ) ;
#99200=EDGE_CURVE ( 'NONE', #34748, #75985, #57847, .T. ) ;
#99396=DIRECTION ( 'NONE',  ( -1.000000000000000000, 0.000000000000000000, 0.000000000000000000 ) ) ;
#99403=ADVANCED_FACE ( 'NONE', ( #34694 ), #92346, .F. ) ;
#99415=CARTESIAN_POINT ( 'NONE',  ( -3.400000000000000355, 4.163799117101001052E-16, -8.000000000000000000 ) ) ;
#99533=CARTESIAN_POINT ( 'NONE',  ( -5.416666666666666075, -4.378239541354687070, -5.848636054922041971 ) ) ;
#99551=DIRECTION ( 'NONE',  ( -0.000000000000000000, -0.000000000000000000, 1.000000000000000000 ) ) ;
#99565=VECTOR ( 'NONE', #46994, 1000.000000000000000 ) ;
#99591=CARTESIAN_POINT ( 'NONE',  ( 3.340000000000000746, 0.000000000000000000, -0.4621369752184079083 ) ) ;
#99665=AXIS2_PLACEMENT_3D ( 'NONE', #33891, #41414, #384 ) ;
#99680=CARTESIAN_POINT ( 'NONE',  ( -5.979512004945808812, 4.053280633787061937, -0.5609245978742136707 ) ) ;
#99689=ORIENTED_EDGE ( 'NONE', *, *, #52701, .T. ) ;
#99993=DIRECTION ( 'NONE',  ( 0.000000000000000000, 0.000000000000000000, 1.000000000000000000 ) ) ;
#100004=CONICAL_SURFACE ( 'NONE', #29378, 3.340000000000000746, 0.9599310885968781459 ) ;
#100068=ORIENTED_EDGE ( 'NONE', *, *, #15002, .T. ) ;
#100073=DIRECTION ( 'NONE',  ( -1.000000000000000000, 0.000000000000000000, 0.000000000000000000 ) ) ;
#100140=CARTESIAN_POINT ( 'NONE',  ( -4.000000000000000000, 0.000000000000000000, -2.296599999999999753 ) ) ;
#100153=CARTESIAN_POINT ( 'NONE',  ( 3.400000000000000355, 0.000000000000000000, -8.000000000000000000 ) ) ;
#100265=VECTOR ( 'NONE', #39714, 1000.000000000000114 ) ;
#100382=CARTESIAN_POINT ( 'NONE',  ( -6.663120783604494335, 3.846954578057034446, -6.460786012260001598 ) ) ;
#100402=EDGE_CURVE ( 'NONE', #15859, #11593, #60605, .T. ) ;
#100453=ORIENTED_EDGE ( 'NONE', *, *, #8549, .T. ) ;
#100473=AXIS2_PLACEMENT_3D ( 'NONE', #42642, #83102, #11320 ) ;
#100475=DIRECTION ( 'NONE',  ( 0.000000000000000000, 0.000000000000000000, 1.000000000000000000 ) ) ;
#100519=CARTESIAN_POINT ( 'NONE',  ( 0.000000000000000000, 0.000000000000000000, -3.852324522925831385 ) ) ;
#100552=DIRECTION ( 'NONE',  ( -1.000000000000000000, 0.000000000000000000, 0.000000000000000000 ) ) ;
#100571=DIRECTION ( 'NONE',  ( -1.000000000000000000, 0.000000000000000000, 0.000000000000000000 ) ) ;
#100575=CARTESIAN_POINT ( 'NONE',  ( 8.331345277524542681, 0.000000000000000000, -7.381345277524544279 ) ) ;
#100632=DIRECTION ( 'NONE',  ( 1.224646799147353207E-16, 1.000000000000000000, 0.000000000000000000 ) ) ;
#100708=EDGE_CURVE ( 'NONE', #29666, #76811, #105851, .T. ) ;
#100756=CARTESIAN_POINT ( 'NONE',  ( 5.699988423468466792, 4.591578518468243608, -6.344710093416083829 ) ) ;
#100772=EDGE_CURVE ( 'NONE', #5468, #84887, #28656, .T. ) ;
#100791=VERTEX_POINT ( 'NONE', #13475 ) ;
#100822=ORIENTED_EDGE ( 'NONE', *, *, #72195, .T. ) ;
#100924=VECTOR ( 'NONE', #11189, 1000.000000000000000 ) ;
#101028=ORIENTED_EDGE ( 'NONE', *, *, #56365, .T. ) ;
#101042=DIRECTION ( 'NONE',  ( -0.000000000000000000, -0.000000000000000000, -1.000000000000000000 ) ) ;
#101066=CARTESIAN_POINT ( 'NONE',  ( 0.000000000000000000, 0.000000000000000000, -4.147675477074182382 ) ) ;
#101068=DIRECTION ( 'NONE',  ( -0.000000000000000000, -0.000000000000000000, -1.000000000000000000 ) ) ;
#101086=EDGE_LOOP ( 'NONE', ( #26272, #50639, #56105, #89524 ) ) ;
#101097=CONICAL_SURFACE ( 'NONE', #23585, 8.542937654374686218, 1.221730476396047704 ) ;
#101176=LINE ( 'NONE', #93624, #32614 ) ;
#101212=ORIENTED_EDGE ( 'NONE', *, *, #87375, .T. ) ;
#101259=CARTESIAN_POINT ( 'NONE',  ( -3.250000000000016431, 5.629165124598842773, 1.734723475976807094E-15 ) ) ;
#101264=VECTOR ( 'NONE', #39974, 1000.000000000000114 ) ;
#101299=ORIENTED_EDGE ( 'NONE', *, *, #49670, .T. ) ;
#101354=EDGE_LOOP ( 'NONE', ( #67260, #27979, #86844, #50585 ) ) ;
#101370=ORIENTED_EDGE ( 'NONE', *, *, #31985, .F. ) ;
#101377=DIRECTION ( 'NONE',  ( -0.5000000000000025535, 0.8660254037844371533, 0.000000000000000000 ) ) ;
#101587=EDGE_CURVE ( 'NONE', #26114, #57008, #102891, .T. ) ;
#101595=ADVANCED_FACE ( 'NONE', ( #58512 ), #23942, .F. ) ;
#101629=ORIENTED_EDGE ( 'NONE', *, *, #75666, .T. ) ;
#101671=EDGE_CURVE ( 'NONE', #102690, #11593, #67201, .T. ) ;
#101698=DIRECTION ( 'NONE',  ( -1.000000000000000000, 0.000000000000000000, 0.000000000000000000 ) ) ;
#101769=CARTESIAN_POINT ( 'NONE',  ( 2.075968632161881544, 6.306992450856642840, -6.056431503345442557 ) ) ;
#102039=DIRECTION ( 'NONE',  ( 0.000000000000000000, 0.000000000000000000, 1.000000000000000000 ) ) ;
#102186=DIRECTION ( 'NONE',  ( 0.000000000000000000, 0.000000000000000000, 1.000000000000000000 ) ) ;
#102202=EDGE_CURVE ( 'NONE', #74698, #75985, #44539, .T. ) ;
#102239=DIRECTION ( 'NONE',  ( -1.000000000000000000, 0.000000000000000000, 0.000000000000000000 ) ) ;
#102248=ORIENTED_EDGE ( 'NONE', *, *, #74585, .F. ) ;
#102284=PLANE ( 'NONE',  #2812 ) ;
#102314=CARTESIAN_POINT ( 'NONE',  ( -4.466912950640278268E-14, -7.505553499465147382, -0.7999999999999977129 ) ) ;
#102355=VERTEX_POINT ( 'NONE', #67474 ) ;
#102421=EDGE_LOOP ( 'NONE', ( #74773, #84487, #19678, #36099 ) ) ;
#102433=ORIENTED_EDGE ( 'NONE', *, *, #8662, .T. ) ;
#102468=CARTESIAN_POINT ( 'NONE',  ( 0.000000000000000000, 0.000000000000000000, -1.581124522925831499 ) ) ;
#102558=CARTESIAN_POINT ( 'NONE',  ( 0.000000000000000000, 0.000000000000000000, -8.000000000000000000 ) ) ;
#102559=AXIS2_PLACEMENT_3D ( 'NONE', #96385, #38167, #5757 ) ;
#102561=ORIENTED_EDGE ( 'NONE', *, *, #14296, .F. ) ;
#102565=CARTESIAN_POINT ( 'NONE',  ( 6.815830331203682313, -0.6610623347507985637, -6.171384342982605631 ) ) ;
#102578=CARTESIAN_POINT ( 'NONE',  ( 4.000000000000000000, 4.898587196589412829E-16, -5.703399999999999359 ) ) ;
#102630=LINE ( 'NONE', #20709, #45901 ) ;
#102652=FACE_OUTER_BOUND ( 'NONE', #72694, .T. ) ;
#102673=EDGE_CURVE ( 'NONE', #59491, #94655, #10217, .T. ) ;
#102690=VERTEX_POINT ( 'NONE', #76255 ) ;
#102726=DIRECTION ( 'NONE',  ( 1.000000000000000000, 0.000000000000000000, -0.000000000000000000 ) ) ;
#102834=EDGE_LOOP ( 'NONE', ( #15565, #15109, #67530, #67268 ) ) ;
#102882=FACE_BOUND ( 'NONE', #91377, .T. ) ;
#102891=CIRCLE ( 'NONE', #32230, 3.400000000000000355 ) ;
#102954=VERTEX_POINT ( 'NONE', #29612 ) ;
#102998=ORIENTED_EDGE ( 'NONE', *, *, #70339, .F. ) ;
#103002=AXIS2_PLACEMENT_3D ( 'NONE', #73022, #1245, #83780 ) ;
#103027=ORIENTED_EDGE ( 'NONE', *, *, #87585, .T. ) ;
#103085=EDGE_LOOP ( 'NONE', ( #17417, #97141, #65633, #58140 ) ) ;
#103101=CARTESIAN_POINT ( 'NONE',  ( 0.5620262070071395666, -7.564407249984330228, -6.443844059477459751 ) ) ;
#103105=CARTESIAN_POINT ( 'NONE',  ( 1.860380241283026592, 6.431462466365327479, -0.1499059597315286207 ) ) ;
#103172=CARTESIAN_POINT ( 'NONE',  ( 6.499999999999999112, 3.752776749732559036, -8.000000000000000000 ) ) ;
#103257=FACE_BOUND ( 'NONE', #57696, .T. ) ;
#103278=CARTESIAN_POINT ( 'NONE',  ( 0.000000000000000000, 0.000000000000000000, -4.567799999999999194 ) ) ;
#103288=ADVANCED_FACE ( 'NONE', ( #13902 ), #79713, .F. ) ;
#103334=DIRECTION ( 'NONE',  ( -0.8191520442889881348, 1.003171929053520186E-16, 0.5735764363510513775 ) ) ;
#103346=DIRECTION ( 'NONE',  ( 0.000000000000000000, 0.000000000000000000, 1.000000000000000000 ) ) ;
#103369=SURFACE_STYLE_FILL_AREA ( #69416 ) ;
#103446=DIRECTION ( 'NONE',  ( -1.000000000000000000, 0.000000000000000000, 0.000000000000000000 ) ) ;
#103456=AXIS2_PLACEMENT_3D ( 'NONE', #17299, #83075, #18368 ) ;
#103498=FACE_OUTER_BOUND ( 'NONE', #106192, .T. ) ;
#103506=CONICAL_SURFACE ( 'NONE', #31175, 6.500000000000000888, 0.8987552595851637793 ) ;
#103510=DIRECTION ( 'NONE',  ( -1.000000000000000000, 0.000000000000000000, 0.000000000000000000 ) ) ;
#103540=CARTESIAN_POINT ( 'NONE',  ( 6.539198257602121700, 3.775407874310910739, -6.286450516131048438 ) ) ;
#103568=CARTESIAN_POINT ( 'NONE',  ( 3.400000000000000355, 0.000000000000000000, -4.987924522925830217 ) ) ;
#103610=VECTOR ( 'NONE', #62592, 1000.000000000000000 ) ;
#103617=EDGE_CURVE ( 'NONE', #18245, #95748, #53573, .T. ) ;
#103618=LINE ( 'NONE', #62130, #17052 ) ;
#103626=FACE_OUTER_BOUND ( 'NONE', #12644, .T. ) ;
#103646=CARTESIAN_POINT ( 'NONE',  ( -2.352990130084491319E-16, 7.505553499465148271, -6.064240316920404439 ) ) ;
#103660=DIRECTION ( 'NONE',  ( 0.000000000000000000, 0.000000000000000000, 1.000000000000000000 ) ) ;
#103785=CARTESIAN_POINT ( 'NONE',  ( -4.424031367838773932, 4.951337798340085250, -6.056431503345439005 ) ) ;
#103825=CARTESIAN_POINT ( 'NONE',  ( 8.331345277524542681, 0.000000000000000000, -8.000000000000000000 ) ) ;
#103829=LINE ( 'NONE', #88189, #87446 ) ;
#103859=ORIENTED_EDGE ( 'NONE', *, *, #31985, .T. ) ;
#103884=CARTESIAN_POINT ( 'NONE',  ( 6.725979247667768668, 3.622307570260303144, -6.470294263593357798 ) ) ;
#103900=DIRECTION ( 'NONE',  ( -0.000000000000000000, -0.000000000000000000, -1.000000000000000000 ) ) ;
#103958=CARTESIAN_POINT ( 'NONE',  ( 0.000000000000000000, 0.000000000000000000, -7.974599999999995248 ) ) ;
#104075=EDGE_CURVE ( 'NONE', #56514, #35363, #36079, .T. ) ;
#104276=VECTOR ( 'NONE', #15813, 1000.000000000000114 ) ;
#104376=LINE ( 'NONE', #37037, #38149 ) ;
#104419=CARTESIAN_POINT ( 'NONE',  ( -3.983107665916332252, 5.570601890521282407, -6.171481112545252223 ) ) ;
#104447=ADVANCED_FACE ( 'NONE', ( #5748 ), #69144, .F. ) ;
#104580=LINE ( 'NONE', #12905, #33889 ) ;
#104614=CONICAL_SURFACE ( 'NONE', #87395, 4.000000000000000000, 0.9599310885968912466 ) ;
#104623=DIRECTION ( 'NONE',  ( -0.8191520442889974607, 0.000000000000000000, -0.5735764363510379438 ) ) ;
#104660=ORIENTED_EDGE ( 'NONE', *, *, #52977, .F. ) ;
#104711=CARTESIAN_POINT ( 'NONE',  ( 6.815830331203684977, 1.210606185736183200E-13, -6.171384342982610072 ) ) ;
#104738=ORIENTED_EDGE ( 'NONE', *, *, #21556, .F. ) ;
#104748=VERTEX_POINT ( 'NONE', #62293 ) ;
#104802=ADVANCED_FACE ( 'NONE', ( #88149 ), #20510, .F. ) ;
#104804=AXIS2_PLACEMENT_3D ( 'NONE', #47970, #6988, #39907 ) ;
#104820=AXIS2_PLACEMENT_3D ( 'NONE', #102468, #84687, #28615 ) ;
#104891=CIRCLE ( 'NONE', #30848, 3.400000000000000355 ) ;
#104999=ADVANCED_FACE ( 'NONE', ( #93982 ), #58961, .F. ) ;
#105000=CARTESIAN_POINT ( 'NONE',  ( -3.400000000000000355, 4.163799117101001052E-16, -3.012075477074183105 ) ) ;
#105012=EDGE_CURVE ( 'NONE', #18921, #11593, #64322, .T. ) ;
#105037=FACE_OUTER_BOUND ( 'NONE', #33573, .T. ) ;
#105093=LINE ( 'NONE', #38260, #12495 ) ;
#105223=ADVANCED_FACE ( 'NONE', ( #65850 ), #8140, .T. ) ;
#105224=ORIENTED_EDGE ( 'NONE', *, *, #103617, .F. ) ;
#105226=CARTESIAN_POINT ( 'NONE',  ( 6.832273232158016185, 3.329759989367381490, -6.449140625371640567 ) ) ;
#105309=ORIENTED_EDGE ( 'NONE', *, *, #47774, .T. ) ;
#105402=CARTESIAN_POINT ( 'NONE',  ( 5.193195059372482212E-16, -7.895640089090903757, -6.564402953523731377 ) ) ;
#105461=CARTESIAN_POINT ( 'NONE',  ( 0.000000000000000000, 0.000000000000000000, -2.716724522925831220 ) ) ;
#105590=DIRECTION ( 'NONE',  ( -1.000000000000000000, 0.000000000000000000, 0.000000000000000000 ) ) ;
#105599=CIRCLE ( 'NONE', #45333, 3.981862520314373377 ) ;
#105746=CARTESIAN_POINT ( 'NONE',  ( 6.499999999999998224, -4.012858516023022126, -6.470130706010832178 ) ) ;
#105851=B_SPLINE_CURVE_WITH_KNOTS ( 'NONE', 3,
 ( #98766, #73427, #17356, #1117, #46, #50230 ),
 .UNSPECIFIED., .F., .F.,
 ( 4, 2, 4 ),
 ( 0.003841072314098388854, 0.005765657563962199410, 0.007690242813826009965 ),
 .UNSPECIFIED. ) ;
#105883=CARTESIAN_POINT ( 'NONE',  ( 3.250000000000015099, 5.629165124598843661, 1.734723475976807094E-15 ) ) ;
#105906=DIRECTION ( 'NONE',  ( -0.000000000000000000, -0.000000000000000000, -1.000000000000000000 ) ) ;
#105964=ORIENTED_EDGE ( 'NONE', *, *, #71142, .T. ) ;
#105976=DIRECTION ( 'NONE',  ( -1.000000000000000000, 0.000000000000000000, 0.000000000000000000 ) ) ;
#105977=CARTESIAN_POINT ( 'NONE',  ( -6.500000000000000000, -3.752776749732588346, -6.177802698399963433 ) ) ;
#106026=CARTESIAN_POINT ( 'NONE',  ( 1.098735407078442972, -7.248058225758801321, -6.326622577870249842 ) ) ;
#106133=DIRECTION ( 'NONE',  ( 1.000000000000000000, 0.000000000000000000, 0.000000000000000000 ) ) ;
#106144=CONICAL_SURFACE ( 'NONE', #64818, 4.000000000000000000, 0.9599310885968912466 ) ;
#106192=EDGE_LOOP ( 'NONE', ( #65986, #88949, #41253, #67096, #67101 ) ) ;
#106261=CARTESIAN_POINT ( 'NONE',  ( 6.499999999999999112, 3.402385889607431046, -5.998095356498420294 ) ) ;
#106267=ADVANCED_FACE ( 'NONE', ( #18962 ), #81249, .F. ) ;
#106334=LINE ( 'NONE', #75031, #37556 ) ;
#106421=CARTESIAN_POINT ( 'NONE',  ( 8.673617379884035472E-16, 7.505553499465148271, -0.7999999999999977129 ) ) ;
#106496=DIRECTION ( 'NONE',  ( 0.000000000000000000, 0.000000000000000000, 1.000000000000000000 ) ) ;
#106567=CARTESIAN_POINT ( 'NONE',  ( 5.619193549421241052, -4.261310591078192545, -5.875704392893802641 ) ) ;
#106657=CARTESIAN_POINT ( 'NONE',  ( -6.499999999999999112, 3.752776749732556816, -6.064240316920397333 ) ) ;
#106661=ORIENTED_EDGE ( 'NONE', *, *, #86082, .T. ) ;
#106680=DIRECTION ( 'NONE',  ( -1.000000000000000000, 0.000000000000000000, 0.000000000000000000 ) ) ;
#106749=EDGE_LOOP ( 'NONE', ( #79340, #12594, #64870, #20560, #45820 ) ) ;
ENDSEC;
END-ISO-10303-21;
